ISO-10303-21;
HEADER;
/* Generated by software containing ST-Developer
 * from STEP Tools, Inc. (www.steptools.com) 
 */

FILE_DESCRIPTION(
/* description */ ('Ball-race swivel caster'),
/* implementation_level */ '2;1');

FILE_NAME(
/* name */ 'Shaft washer.step',
/* time_stamp */ '2026-10-29T16:15:51-07:00',
/* author */ (''),
/* organization */ (''),
/* preprocessor_version */ 'ST-DEVELOPER v20.2',
/* originating_system */ 'Autodesk Translation Framework v15.17.0.0',
/* authorisation */ '');

FILE_SCHEMA (('AUTOMOTIVE_DESIGN { 1 0 10303 214 3 1 1 }'));
ENDSEC;

DATA;
#10=MECHANICAL_DESIGN_GEOMETRIC_PRESENTATION_REPRESENTATION('',(#300),#7816);
#170=TOROIDAL_SURFACE('',#4062,1.1,0.208);
#171=TOROIDAL_SURFACE('',#4064,1.1,0.208);
#172=TOROIDAL_SURFACE('',#4066,1.1,0.208);
#173=TOROIDAL_SURFACE('',#4068,1.1,0.208);
#174=TOROIDAL_SURFACE('',#4070,1.1,0.208);
#175=TOROIDAL_SURFACE('',#4072,1.1,0.208);
#176=TOROIDAL_SURFACE('',#4074,1.1,0.208);
#177=TOROIDAL_SURFACE('',#4076,1.1,0.208);
#178=TOROIDAL_SURFACE('',#4078,1.1,0.208);
#179=TOROIDAL_SURFACE('',#4080,1.1,0.208);
#192=B_SPLINE_CURVE_WITH_KNOTS('',3,(#5795,#5796,#5797,#5798,#5799,#5800,
#5801,#5802,#5803,#5804),.UNSPECIFIED.,.F.,.F.,(4,2,2,2,4),(-0.464072133285151,
-0.409463462974798,-0.35465357795961,-0.295254131517933,-0.285596349669134),
 .UNSPECIFIED.);
#193=B_SPLINE_CURVE_WITH_KNOTS('',3,(#5808,#5809,#5810,#5811,#5812,#5813,
#5814,#5815,#5816,#5817,#5818,#5819,#5820,#5821,#5822,#5823),
 .UNSPECIFIED.,.F.,.F.,(4,2,2,2,2,2,2,4),(-0.45417904189248,-0.395759356749822,
-0.338728191012566,-0.275894647345884,-0.221135020913429,-0.164911408034045,
-0.0984111283989842,0.),.UNSPECIFIED.);
#194=B_SPLINE_CURVE_WITH_KNOTS('',3,(#5826,#5827,#5828,#5829,#5830,#5831,
#5832,#5833,#5834,#5835),.UNSPECIFIED.,.F.,.F.,(4,2,2,2,4),(-0.285596349669134,
-0.239649525441968,-0.179869516594422,-0.105654793183186,0.),
 .UNSPECIFIED.);
#195=B_SPLINE_CURVE_WITH_KNOTS('',3,(#5844,#5845,#5846,#5847,#5848,#5849,
#5850,#5851,#5852,#5853,#5854,#5855,#5856,#5857,#5858,#5859),
 .UNSPECIFIED.,.F.,.F.,(4,2,2,2,2,2,2,4),(-0.464097123055984,-0.409448749757932,
-0.354953921831336,-0.295351891164135,-0.239773021090731,-0.179990573569022,
-0.105700836781513,0.),.UNSPECIFIED.);
#196=B_SPLINE_CURVE_WITH_KNOTS('',3,(#5863,#5864,#5865,#5866,#5867,#5868,
#5869,#5870,#5871,#5872,#5873,#5874,#5875,#5876,#5877,#5878),
 .UNSPECIFIED.,.F.,.F.,(4,2,2,2,2,2,2,4),(-0.45424830909043,-0.396054469342604,
-0.339406675181722,-0.276261577769454,-0.221379042231552,-0.165164477779452,
-0.098609088443841,0.),.UNSPECIFIED.);
#197=B_SPLINE_CURVE_WITH_KNOTS('',3,(#5888,#5889,#5890,#5891,#5892,#5893,
#5894,#5895,#5896,#5897,#5898,#5899,#5900,#5901,#5902,#5903),
 .UNSPECIFIED.,.F.,.F.,(4,2,2,2,2,2,2,4),(-0.454158667319319,-0.395672852804858,
-0.338529950359415,-0.275786564377704,-0.221062756831308,-0.164836364834591,
-0.0983527839094977,0.),.UNSPECIFIED.);
#198=B_SPLINE_CURVE_WITH_KNOTS('',3,(#5907,#5908,#5909,#5910,#5911,#5912,
#5913,#5914,#5915,#5916,#5917,#5918,#5919,#5920,#5921,#5922),
 .UNSPECIFIED.,.F.,.F.,(4,2,2,2,2,2,2,4),(-0.46406483796248,-0.409466852189161,
-0.354565796864805,-0.295225270188452,-0.239612954364848,-0.179833767169889,
-0.105641391458423,0.),.UNSPECIFIED.);
#199=B_SPLINE_CURVE_WITH_KNOTS('',3,(#5930,#5931,#5932,#5933,#5934,#5935,
#5936,#5937),.UNSPECIFIED.,.F.,.F.,(4,2,2,4),(-0.454179041892498,-0.395759356749834,
-0.338728191012573,-0.307335875219019),.UNSPECIFIED.);
#200=B_SPLINE_CURVE_WITH_KNOTS('',3,(#5941,#5942,#5943,#5944,#5945,#5946,
#5947,#5948,#5949,#5950,#5951,#5952,#5953,#5954,#5955,#5956),
 .UNSPECIFIED.,.F.,.F.,(4,2,2,2,2,2,2,4),(-0.464072133285143,-0.40946346297479,
-0.354653577959605,-0.295254131517927,-0.239649525441963,-0.179869516594418,
-0.105654793183184,0.),.UNSPECIFIED.);
#201=B_SPLINE_CURVE_WITH_KNOTS('',3,(#5959,#5960,#5961,#5962,#5963,#5964,
#5965,#5966,#5967,#5968,#5969,#5970),.UNSPECIFIED.,.F.,.F.,(4,2,2,2,2,4),
(-0.307335875219019,-0.275894647345887,-0.221135020913433,-0.16491140803405,
-0.0984111283989864,0.),.UNSPECIFIED.);
#202=B_SPLINE_CURVE_WITH_KNOTS('',3,(#5977,#5978,#5979,#5980,#5981,#5982,
#5983,#5984,#5985,#5986,#5987,#5988,#5989,#5990,#5991,#5992),
 .UNSPECIFIED.,.F.,.F.,(4,2,2,2,2,2,2,4),(-0.454248309090363,-0.396054469342546,
-0.339406675181674,-0.276261577769416,-0.221379042231522,-0.16516447777943,
-0.0986090884438293,-0.028880024024463),.UNSPECIFIED.);
#203=B_SPLINE_CURVE_WITH_KNOTS('',3,(#5996,#5997,#5998,#5999,#6000,#6001,
#6002,#6003,#6004,#6005,#6006,#6007,#6008,#6009,#6010,#6011),
 .UNSPECIFIED.,.F.,.F.,(4,2,2,2,2,2,2,4),(-0.464097123056143,-0.409448749758071,
-0.354953921831454,-0.29535189116423,-0.239773021090806,-0.179990573569076,
-0.10570083678154,0.),.UNSPECIFIED.);
#204=B_SPLINE_CURVE_WITH_KNOTS('',3,(#6014,#6015,#6016,#6017),
 .UNSPECIFIED.,.F.,.F.,(4,4),(-0.028880024024463,0.),.UNSPECIFIED.);
#205=B_SPLINE_CURVE_WITH_KNOTS('',3,(#6024,#6025,#6026,#6027,#6028,#6029,
#6030,#6031,#6032,#6033,#6034,#6035),.UNSPECIFIED.,.F.,.F.,(4,2,2,2,2,4),
(-0.45417904189259,-0.395759356749914,-0.338728191012644,-0.275894647345943,
-0.221135020913473,-0.178087805736112),.UNSPECIFIED.);
#206=B_SPLINE_CURVE_WITH_KNOTS('',3,(#6039,#6040,#6041,#6042,#6043,#6044,
#6045,#6046,#6047,#6048,#6049,#6050,#6051,#6052,#6053,#6054),
 .UNSPECIFIED.,.F.,.F.,(4,2,2,2,2,2,2,4),(-0.464072133285183,-0.409463462974824,
-0.35465357795963,-0.295254131517949,-0.239649525441983,-0.179869516594434,
-0.10565479318319,0.),.UNSPECIFIED.);
#207=B_SPLINE_CURVE_WITH_KNOTS('',3,(#6057,#6058,#6059,#6060,#6061,#6062,
#6063,#6064),.UNSPECIFIED.,.F.,.F.,(4,2,2,4),(-0.178087805736112,-0.164911408034076,
-0.098411128398999,0.),.UNSPECIFIED.);
#208=B_SPLINE_CURVE_WITH_KNOTS('',3,(#6073,#6074,#6075,#6076,#6077,#6078,
#6079,#6080,#6081,#6082,#6083,#6084,#6085,#6086,#6087,#6088),
 .UNSPECIFIED.,.F.,.F.,(4,2,2,2,2,2,2,4),(-0.464097123055936,-0.409448749757892,
-0.354953921831303,-0.295351891164108,-0.239773021090708,-0.179990573569004,
-0.105700836781506,0.),.UNSPECIFIED.);
#209=B_SPLINE_CURVE_WITH_KNOTS('',3,(#6092,#6093,#6094,#6095,#6096,#6097,
#6098,#6099,#6100,#6101,#6102,#6103,#6104,#6105,#6106,#6107),
 .UNSPECIFIED.,.F.,.F.,(4,2,2,2,2,2,2,4),(-0.454248309090378,-0.396054469342558,
-0.339406675181681,-0.276261577769421,-0.221379042231525,-0.165164477779432,
-0.0986090884438326,0.),.UNSPECIFIED.);
#210=B_SPLINE_CURVE_WITH_KNOTS('',3,(#6117,#6118,#6119,#6120,#6121,#6122,
#6123,#6124,#6125,#6126,#6127,#6128,#6129,#6130,#6131,#6132),
 .UNSPECIFIED.,.F.,.F.,(4,2,2,2,2,2,2,4),(-0.464064837962455,-0.409466852189138,
-0.354565796864784,-0.295225270188435,-0.239612954364835,-0.17983376716988,
-0.105641391458419,0.),.UNSPECIFIED.);
#211=B_SPLINE_CURVE_WITH_KNOTS('',3,(#6136,#6137,#6138,#6139,#6140,#6141,
#6142,#6143,#6144,#6145,#6146,#6147,#6148,#6149,#6150,#6151),
 .UNSPECIFIED.,.F.,.F.,(4,2,2,2,2,2,2,4),(-0.454158667319288,-0.395672852804831,
-0.338529950359391,-0.275786564377685,-0.221062756831291,-0.164836364834576,
-0.0983527839094893,0.),.UNSPECIFIED.);
#212=B_SPLINE_CURVE_WITH_KNOTS('',3,(#6159,#6160,#6161,#6162,#6163,#6164,
#6165,#6166,#6167,#6168,#6169,#6170,#6171,#6172),.UNSPECIFIED.,.F.,.F.,
(4,2,2,2,2,2,4),(-0.464072133285276,-0.409463462974907,-0.354653577959703,
-0.295254131518009,-0.239649525442028,-0.179869516594465,-0.153354495923179),
 .UNSPECIFIED.);
#213=B_SPLINE_CURVE_WITH_KNOTS('',3,(#6176,#6177,#6178,#6179,#6180,#6181,
#6182,#6183,#6184,#6185,#6186,#6187,#6188,#6189,#6190,#6191),
 .UNSPECIFIED.,.F.,.F.,(4,2,2,2,2,2,2,4),(-0.454179041892453,-0.395759356749796,
-0.338728191012541,-0.275894647345861,-0.221135020913411,-0.164911408034033,
-0.0984111283989789,0.),.UNSPECIFIED.);
#214=B_SPLINE_CURVE_WITH_KNOTS('',3,(#6194,#6195,#6196,#6197,#6198,#6199),
 .UNSPECIFIED.,.F.,.F.,(4,2,4),(-0.153354495923179,-0.105654793183204,0.),
 .UNSPECIFIED.);
#215=B_SPLINE_CURVE_WITH_KNOTS('',3,(#6206,#6207,#6208,#6209),
 .UNSPECIFIED.,.F.,.F.,(4,4),(-0.464097123055962,-0.436632642152651),
 .UNSPECIFIED.);
#216=B_SPLINE_CURVE_WITH_KNOTS('',3,(#6213,#6214,#6215,#6216,#6217,#6218,
#6219,#6220,#6221,#6222,#6223,#6224,#6225,#6226,#6227,#6228),
 .UNSPECIFIED.,.F.,.F.,(4,2,2,2,2,2,2,4),(-0.45424830909032,-0.396054469342508,
-0.33940667518164,-0.27626157776939,-0.221379042231501,-0.165164477779415,
-0.0986090884438244,0.),.UNSPECIFIED.);
#217=B_SPLINE_CURVE_WITH_KNOTS('',3,(#6231,#6232,#6233,#6234,#6235,#6236,
#6237,#6238,#6239,#6240,#6241,#6242,#6243,#6244,#6245,#6246),
 .UNSPECIFIED.,.F.,.F.,(4,2,2,2,2,2,2,4),(-0.436632642152651,-0.409448749757915,
-0.354953921831322,-0.295351891164124,-0.239773021090723,-0.179990573569017,
-0.105700836781513,0.),.UNSPECIFIED.);
#260=SHAPE_REPRESENTATION_RELATIONSHIP('SRR','None',#7906,#280);
#280=ADVANCED_BREP_SHAPE_REPRESENTATION('',(#336),#7795);
#300=STYLED_ITEM('',(#8104),#336);
#336=MANIFOLD_SOLID_BREP('Body1',#3706);
#382=FACE_BOUND('',#777,.T.);
#383=FACE_BOUND('',#789,.T.);
#384=FACE_BOUND('',#792,.T.);
#385=FACE_BOUND('',#793,.T.);
#386=FACE_BOUND('',#794,.T.);
#387=FACE_BOUND('',#795,.T.);
#388=FACE_BOUND('',#796,.T.);
#389=FACE_BOUND('',#797,.T.);
#390=FACE_BOUND('',#798,.T.);
#391=FACE_BOUND('',#799,.T.);
#392=FACE_BOUND('',#800,.T.);
#393=FACE_BOUND('',#801,.T.);
#394=FACE_BOUND('',#802,.T.);
#449=PLANE('',#4050);
#450=PLANE('',#4082);
#451=PLANE('',#4086);
#544=FACE_OUTER_BOUND('',#766,.T.);
#545=FACE_OUTER_BOUND('',#767,.T.);
#546=FACE_OUTER_BOUND('',#768,.T.);
#547=FACE_OUTER_BOUND('',#769,.T.);
#548=FACE_OUTER_BOUND('',#770,.T.);
#549=FACE_OUTER_BOUND('',#771,.T.);
#550=FACE_OUTER_BOUND('',#772,.T.);
#551=FACE_OUTER_BOUND('',#773,.T.);
#552=FACE_OUTER_BOUND('',#774,.T.);
#553=FACE_OUTER_BOUND('',#775,.T.);
#554=FACE_OUTER_BOUND('',#776,.T.);
#555=FACE_OUTER_BOUND('',#778,.T.);
#556=FACE_OUTER_BOUND('',#779,.T.);
#557=FACE_OUTER_BOUND('',#780,.T.);
#558=FACE_OUTER_BOUND('',#781,.T.);
#559=FACE_OUTER_BOUND('',#782,.T.);
#560=FACE_OUTER_BOUND('',#783,.T.);
#561=FACE_OUTER_BOUND('',#784,.T.);
#562=FACE_OUTER_BOUND('',#785,.T.);
#563=FACE_OUTER_BOUND('',#786,.T.);
#564=FACE_OUTER_BOUND('',#787,.T.);
#565=FACE_OUTER_BOUND('',#788,.T.);
#566=FACE_OUTER_BOUND('',#790,.T.);
#567=FACE_OUTER_BOUND('',#791,.T.);
#568=FACE_OUTER_BOUND('',#803,.T.);
#766=EDGE_LOOP('',(#2511,#2512,#2513,#2514,#2515,#2516,#2517,#2518));
#767=EDGE_LOOP('',(#2519,#2520,#2521,#2522,#2523,#2524,#2525,#2526));
#768=EDGE_LOOP('',(#2527,#2528,#2529,#2530,#2531,#2532,#2533,#2534));
#769=EDGE_LOOP('',(#2535,#2536,#2537,#2538,#2539,#2540,#2541,#2542));
#770=EDGE_LOOP('',(#2543,#2544,#2545,#2546,#2547,#2548,#2549,#2550));
#771=EDGE_LOOP('',(#2551,#2552,#2553,#2554,#2555,#2556,#2557,#2558));
#772=EDGE_LOOP('',(#2559,#2560,#2561,#2562,#2563,#2564,#2565,#2566));
#773=EDGE_LOOP('',(#2567,#2568,#2569,#2570,#2571,#2572,#2573,#2574));
#774=EDGE_LOOP('',(#2575,#2576,#2577,#2578,#2579,#2580,#2581,#2582));
#775=EDGE_LOOP('',(#2583,#2584,#2585,#2586,#2587,#2588,#2589,#2590));
#776=EDGE_LOOP('',(#2591,#2592,#2593,#2594,#2595,#2596,#2597,#2598,#2599,
#2600,#2601,#2602,#2603,#2604,#2605,#2606,#2607,#2608,#2609,#2610,#2611));
#777=EDGE_LOOP('',(#2612));
#778=EDGE_LOOP('',(#2613,#2614,#2615,#2616));
#779=EDGE_LOOP('',(#2617,#2618,#2619,#2620,#2621));
#780=EDGE_LOOP('',(#2622,#2623,#2624,#2625,#2626));
#781=EDGE_LOOP('',(#2627,#2628,#2629,#2630,#2631));
#782=EDGE_LOOP('',(#2632,#2633,#2634,#2635));
#783=EDGE_LOOP('',(#2636,#2637,#2638,#2639));
#784=EDGE_LOOP('',(#2640,#2641,#2642,#2643,#2644));
#785=EDGE_LOOP('',(#2645,#2646,#2647,#2648));
#786=EDGE_LOOP('',(#2649,#2650,#2651,#2652,#2653));
#787=EDGE_LOOP('',(#2654,#2655,#2656,#2657,#2658));
#788=EDGE_LOOP('',(#2659));
#789=EDGE_LOOP('',(#2660,#2661,#2662,#2663,#2664,#2665,#2666,#2667,#2668,
#2669,#2670,#2671,#2672,#2673,#2674,#2675,#2676,#2677,#2678,#2679,#2680,
#2681,#2682));
#790=EDGE_LOOP('',(#2683,#2684,#2685,#2686));
#791=EDGE_LOOP('',(#2687));
#792=EDGE_LOOP('',(#2688));
#793=EDGE_LOOP('',(#2689));
#794=EDGE_LOOP('',(#2690));
#795=EDGE_LOOP('',(#2691));
#796=EDGE_LOOP('',(#2692));
#797=EDGE_LOOP('',(#2693));
#798=EDGE_LOOP('',(#2694));
#799=EDGE_LOOP('',(#2695));
#800=EDGE_LOOP('',(#2696));
#801=EDGE_LOOP('',(#2697));
#802=EDGE_LOOP('',(#2698));
#803=EDGE_LOOP('',(#2699,#2700,#2701,#2702));
#1032=LINE('',#5793,#1187);
#1033=LINE('',#5840,#1188);
#1034=LINE('',#5884,#1189);
#1035=LINE('',#5928,#1190);
#1036=LINE('',#5975,#1191);
#1037=LINE('',#6022,#1192);
#1038=LINE('',#6069,#1193);
#1039=LINE('',#6113,#1194);
#1040=LINE('',#6157,#1195);
#1041=LINE('',#6204,#1196);
#1042=LINE('',#6286,#1197);
#1043=LINE('',#6291,#1198);
#1187=VECTOR('',#4602,0.22);
#1188=VECTOR('',#4611,0.22);
#1189=VECTOR('',#4622,0.22);
#1190=VECTOR('',#4633,0.22);
#1191=VECTOR('',#4642,0.22);
#1192=VECTOR('',#4651,0.22);
#1193=VECTOR('',#4660,0.22);
#1194=VECTOR('',#4671,0.22);
#1195=VECTOR('',#4682,0.22);
#1196=VECTOR('',#4691,0.22);
#1197=VECTOR('',#4768,1.4);
#1198=VECTOR('',#4775,0.75);
#1339=CIRCLE('',#4007,0.22);
#1340=CIRCLE('',#4008,0.22);
#1341=CIRCLE('',#4009,0.22);
#1342=CIRCLE('',#4011,0.22);
#1343=CIRCLE('',#4012,0.22);
#1344=CIRCLE('',#4013,0.22);
#1345=CIRCLE('',#4014,0.22);
#1346=CIRCLE('',#4016,0.22);
#1347=CIRCLE('',#4017,0.22);
#1348=CIRCLE('',#4018,0.22);
#1349=CIRCLE('',#4019,0.22);
#1350=CIRCLE('',#4021,0.22);
#1351=CIRCLE('',#4022,0.22);
#1352=CIRCLE('',#4023,0.22);
#1353=CIRCLE('',#4025,0.22);
#1354=CIRCLE('',#4026,0.22);
#1355=CIRCLE('',#4027,0.22);
#1356=CIRCLE('',#4029,0.22);
#1357=CIRCLE('',#4030,0.22);
#1358=CIRCLE('',#4031,0.22);
#1359=CIRCLE('',#4033,0.22);
#1360=CIRCLE('',#4034,0.22);
#1361=CIRCLE('',#4035,0.22);
#1362=CIRCLE('',#4036,0.22);
#1363=CIRCLE('',#4038,0.22);
#1364=CIRCLE('',#4039,0.22);
#1365=CIRCLE('',#4040,0.22);
#1366=CIRCLE('',#4041,0.22);
#1367=CIRCLE('',#4043,0.22);
#1368=CIRCLE('',#4044,0.22);
#1369=CIRCLE('',#4045,0.22);
#1370=CIRCLE('',#4047,0.22);
#1371=CIRCLE('',#4048,0.22);
#1372=CIRCLE('',#4049,0.22);
#1373=CIRCLE('',#4051,0.917615790157152);
#1374=CIRCLE('',#4052,0.917615790157152);
#1375=CIRCLE('',#4053,0.917615790157152);
#1376=CIRCLE('',#4054,0.917615790157152);
#1377=CIRCLE('',#4055,0.917615790157152);
#1378=CIRCLE('',#4056,0.917615790157152);
#1379=CIRCLE('',#4057,0.917615790157152);
#1380=CIRCLE('',#4058,0.917615790157152);
#1381=CIRCLE('',#4059,0.917615790157152);
#1382=CIRCLE('',#4060,0.917615790157152);
#1383=CIRCLE('',#4061,0.75);
#1384=CIRCLE('',#4063,1.28238420984285);
#1385=CIRCLE('',#4065,1.28238420984285);
#1386=CIRCLE('',#4067,1.28238420984285);
#1387=CIRCLE('',#4069,1.28238420984285);
#1388=CIRCLE('',#4071,1.28238420984285);
#1389=CIRCLE('',#4073,1.28238420984285);
#1390=CIRCLE('',#4075,1.28238420984285);
#1391=CIRCLE('',#4077,1.28238420984285);
#1392=CIRCLE('',#4079,1.28238420984285);
#1393=CIRCLE('',#4081,1.28238420984285);
#1394=CIRCLE('',#4083,1.4);
#1395=CIRCLE('',#4085,1.4);
#1396=CIRCLE('',#4087,0.75);
#1611=VERTEX_POINT('',#5790);
#1612=VERTEX_POINT('',#5792);
#1613=VERTEX_POINT('',#5794);
#1614=VERTEX_POINT('',#5805);
#1615=VERTEX_POINT('',#5807);
#1616=VERTEX_POINT('',#5824);
#1617=VERTEX_POINT('',#5837);
#1618=VERTEX_POINT('',#5839);
#1619=VERTEX_POINT('',#5841);
#1620=VERTEX_POINT('',#5843);
#1621=VERTEX_POINT('',#5860);
#1622=VERTEX_POINT('',#5862);
#1623=VERTEX_POINT('',#5881);
#1624=VERTEX_POINT('',#5883);
#1625=VERTEX_POINT('',#5885);
#1626=VERTEX_POINT('',#5887);
#1627=VERTEX_POINT('',#5904);
#1628=VERTEX_POINT('',#5906);
#1629=VERTEX_POINT('',#5925);
#1630=VERTEX_POINT('',#5927);
#1631=VERTEX_POINT('',#5929);
#1632=VERTEX_POINT('',#5938);
#1633=VERTEX_POINT('',#5940);
#1634=VERTEX_POINT('',#5957);
#1635=VERTEX_POINT('',#5972);
#1636=VERTEX_POINT('',#5974);
#1637=VERTEX_POINT('',#5976);
#1638=VERTEX_POINT('',#5993);
#1639=VERTEX_POINT('',#5995);
#1640=VERTEX_POINT('',#6012);
#1641=VERTEX_POINT('',#6019);
#1642=VERTEX_POINT('',#6021);
#1643=VERTEX_POINT('',#6023);
#1644=VERTEX_POINT('',#6036);
#1645=VERTEX_POINT('',#6038);
#1646=VERTEX_POINT('',#6055);
#1647=VERTEX_POINT('',#6066);
#1648=VERTEX_POINT('',#6068);
#1649=VERTEX_POINT('',#6070);
#1650=VERTEX_POINT('',#6072);
#1651=VERTEX_POINT('',#6089);
#1652=VERTEX_POINT('',#6091);
#1653=VERTEX_POINT('',#6110);
#1654=VERTEX_POINT('',#6112);
#1655=VERTEX_POINT('',#6114);
#1656=VERTEX_POINT('',#6116);
#1657=VERTEX_POINT('',#6133);
#1658=VERTEX_POINT('',#6135);
#1659=VERTEX_POINT('',#6154);
#1660=VERTEX_POINT('',#6156);
#1661=VERTEX_POINT('',#6158);
#1662=VERTEX_POINT('',#6173);
#1663=VERTEX_POINT('',#6175);
#1664=VERTEX_POINT('',#6192);
#1665=VERTEX_POINT('',#6201);
#1666=VERTEX_POINT('',#6203);
#1667=VERTEX_POINT('',#6205);
#1668=VERTEX_POINT('',#6210);
#1669=VERTEX_POINT('',#6212);
#1670=VERTEX_POINT('',#6229);
#1671=VERTEX_POINT('',#6258);
#1672=VERTEX_POINT('',#6281);
#1673=VERTEX_POINT('',#6284);
#1674=VERTEX_POINT('',#6288);
#1975=EDGE_CURVE('',#1611,#1611,#1339,.T.);
#1976=EDGE_CURVE('',#1611,#1612,#1032,.T.);
#1977=EDGE_CURVE('',#1613,#1612,#192,.T.);
#1978=EDGE_CURVE('',#1614,#1613,#1340,.T.);
#1979=EDGE_CURVE('',#1615,#1614,#193,.T.);
#1980=EDGE_CURVE('',#1616,#1615,#1341,.T.);
#1981=EDGE_CURVE('',#1612,#1616,#194,.T.);
#1982=EDGE_CURVE('',#1617,#1617,#1342,.T.);
#1983=EDGE_CURVE('',#1617,#1618,#1033,.T.);
#1984=EDGE_CURVE('',#1619,#1618,#1343,.T.);
#1985=EDGE_CURVE('',#1620,#1619,#195,.T.);
#1986=EDGE_CURVE('',#1621,#1620,#1344,.T.);
#1987=EDGE_CURVE('',#1622,#1621,#196,.T.);
#1988=EDGE_CURVE('',#1618,#1622,#1345,.T.);
#1989=EDGE_CURVE('',#1623,#1623,#1346,.T.);
#1990=EDGE_CURVE('',#1623,#1624,#1034,.T.);
#1991=EDGE_CURVE('',#1625,#1624,#1347,.T.);
#1992=EDGE_CURVE('',#1626,#1625,#197,.T.);
#1993=EDGE_CURVE('',#1627,#1626,#1348,.T.);
#1994=EDGE_CURVE('',#1628,#1627,#198,.T.);
#1995=EDGE_CURVE('',#1624,#1628,#1349,.T.);
#1996=EDGE_CURVE('',#1629,#1629,#1350,.T.);
#1997=EDGE_CURVE('',#1629,#1630,#1035,.T.);
#1998=EDGE_CURVE('',#1631,#1630,#199,.T.);
#1999=EDGE_CURVE('',#1632,#1631,#1351,.T.);
#2000=EDGE_CURVE('',#1633,#1632,#200,.T.);
#2001=EDGE_CURVE('',#1634,#1633,#1352,.T.);
#2002=EDGE_CURVE('',#1630,#1634,#201,.T.);
#2003=EDGE_CURVE('',#1635,#1635,#1353,.T.);
#2004=EDGE_CURVE('',#1635,#1636,#1036,.T.);
#2005=EDGE_CURVE('',#1637,#1636,#202,.T.);
#2006=EDGE_CURVE('',#1638,#1637,#1354,.T.);
#2007=EDGE_CURVE('',#1639,#1638,#203,.T.);
#2008=EDGE_CURVE('',#1640,#1639,#1355,.T.);
#2009=EDGE_CURVE('',#1636,#1640,#204,.T.);
#2010=EDGE_CURVE('',#1641,#1641,#1356,.T.);
#2011=EDGE_CURVE('',#1641,#1642,#1037,.T.);
#2012=EDGE_CURVE('',#1643,#1642,#205,.T.);
#2013=EDGE_CURVE('',#1644,#1643,#1357,.T.);
#2014=EDGE_CURVE('',#1645,#1644,#206,.T.);
#2015=EDGE_CURVE('',#1646,#1645,#1358,.T.);
#2016=EDGE_CURVE('',#1642,#1646,#207,.T.);
#2017=EDGE_CURVE('',#1647,#1647,#1359,.T.);
#2018=EDGE_CURVE('',#1647,#1648,#1038,.T.);
#2019=EDGE_CURVE('',#1649,#1648,#1360,.T.);
#2020=EDGE_CURVE('',#1650,#1649,#208,.T.);
#2021=EDGE_CURVE('',#1651,#1650,#1361,.T.);
#2022=EDGE_CURVE('',#1652,#1651,#209,.T.);
#2023=EDGE_CURVE('',#1648,#1652,#1362,.T.);
#2024=EDGE_CURVE('',#1653,#1653,#1363,.T.);
#2025=EDGE_CURVE('',#1653,#1654,#1039,.T.);
#2026=EDGE_CURVE('',#1655,#1654,#1364,.T.);
#2027=EDGE_CURVE('',#1656,#1655,#210,.T.);
#2028=EDGE_CURVE('',#1657,#1656,#1365,.T.);
#2029=EDGE_CURVE('',#1658,#1657,#211,.T.);
#2030=EDGE_CURVE('',#1654,#1658,#1366,.T.);
#2031=EDGE_CURVE('',#1659,#1659,#1367,.T.);
#2032=EDGE_CURVE('',#1659,#1660,#1040,.T.);
#2033=EDGE_CURVE('',#1661,#1660,#212,.T.);
#2034=EDGE_CURVE('',#1662,#1661,#1368,.T.);
#2035=EDGE_CURVE('',#1663,#1662,#213,.T.);
#2036=EDGE_CURVE('',#1664,#1663,#1369,.T.);
#2037=EDGE_CURVE('',#1660,#1664,#214,.T.);
#2038=EDGE_CURVE('',#1665,#1665,#1370,.T.);
#2039=EDGE_CURVE('',#1665,#1666,#1041,.T.);
#2040=EDGE_CURVE('',#1667,#1666,#215,.T.);
#2041=EDGE_CURVE('',#1668,#1667,#1371,.T.);
#2042=EDGE_CURVE('',#1669,#1668,#216,.T.);
#2043=EDGE_CURVE('',#1670,#1669,#1372,.T.);
#2044=EDGE_CURVE('',#1666,#1670,#217,.T.);
#2045=EDGE_CURVE('',#1613,#1662,#1373,.T.);
#2046=EDGE_CURVE('',#1661,#1621,#1374,.T.);
#2047=EDGE_CURVE('',#1620,#1657,#1375,.T.);
#2048=EDGE_CURVE('',#1656,#1651,#1376,.T.);
#2049=EDGE_CURVE('',#1650,#1634,#1377,.T.);
#2050=EDGE_CURVE('',#1633,#1646,#1378,.T.);
#2051=EDGE_CURVE('',#1645,#1640,#1379,.T.);
#2052=EDGE_CURVE('',#1639,#1625,#1380,.T.);
#2053=EDGE_CURVE('',#1628,#1668,#1381,.T.);
#2054=EDGE_CURVE('',#1667,#1614,#1382,.T.);
#2055=EDGE_CURVE('',#1671,#1671,#1383,.T.);
#2056=EDGE_CURVE('',#1652,#1655,#1384,.T.);
#2057=EDGE_CURVE('',#1637,#1644,#1385,.T.);
#2058=EDGE_CURVE('',#1631,#1649,#1386,.T.);
#2059=EDGE_CURVE('',#1643,#1632,#1387,.T.);
#2060=EDGE_CURVE('',#1626,#1638,#1388,.T.);
#2061=EDGE_CURVE('',#1669,#1627,#1389,.T.);
#2062=EDGE_CURVE('',#1622,#1664,#1390,.T.);
#2063=EDGE_CURVE('',#1658,#1619,#1391,.T.);
#2064=EDGE_CURVE('',#1615,#1670,#1392,.T.);
#2065=EDGE_CURVE('',#1663,#1616,#1393,.T.);
#2066=EDGE_CURVE('',#1672,#1672,#1394,.T.);
#2067=EDGE_CURVE('',#1673,#1673,#1395,.T.);
#2068=EDGE_CURVE('',#1673,#1672,#1042,.T.);
#2069=EDGE_CURVE('',#1674,#1674,#1396,.T.);
#2070=EDGE_CURVE('',#1674,#1671,#1043,.T.);
#2511=ORIENTED_EDGE('',*,*,#1975,.F.);
#2512=ORIENTED_EDGE('',*,*,#1976,.T.);
#2513=ORIENTED_EDGE('',*,*,#1977,.F.);
#2514=ORIENTED_EDGE('',*,*,#1978,.F.);
#2515=ORIENTED_EDGE('',*,*,#1979,.F.);
#2516=ORIENTED_EDGE('',*,*,#1980,.F.);
#2517=ORIENTED_EDGE('',*,*,#1981,.F.);
#2518=ORIENTED_EDGE('',*,*,#1976,.F.);
#2519=ORIENTED_EDGE('',*,*,#1982,.F.);
#2520=ORIENTED_EDGE('',*,*,#1983,.T.);
#2521=ORIENTED_EDGE('',*,*,#1984,.F.);
#2522=ORIENTED_EDGE('',*,*,#1985,.F.);
#2523=ORIENTED_EDGE('',*,*,#1986,.F.);
#2524=ORIENTED_EDGE('',*,*,#1987,.F.);
#2525=ORIENTED_EDGE('',*,*,#1988,.F.);
#2526=ORIENTED_EDGE('',*,*,#1983,.F.);
#2527=ORIENTED_EDGE('',*,*,#1989,.F.);
#2528=ORIENTED_EDGE('',*,*,#1990,.T.);
#2529=ORIENTED_EDGE('',*,*,#1991,.F.);
#2530=ORIENTED_EDGE('',*,*,#1992,.F.);
#2531=ORIENTED_EDGE('',*,*,#1993,.F.);
#2532=ORIENTED_EDGE('',*,*,#1994,.F.);
#2533=ORIENTED_EDGE('',*,*,#1995,.F.);
#2534=ORIENTED_EDGE('',*,*,#1990,.F.);
#2535=ORIENTED_EDGE('',*,*,#1996,.F.);
#2536=ORIENTED_EDGE('',*,*,#1997,.T.);
#2537=ORIENTED_EDGE('',*,*,#1998,.F.);
#2538=ORIENTED_EDGE('',*,*,#1999,.F.);
#2539=ORIENTED_EDGE('',*,*,#2000,.F.);
#2540=ORIENTED_EDGE('',*,*,#2001,.F.);
#2541=ORIENTED_EDGE('',*,*,#2002,.F.);
#2542=ORIENTED_EDGE('',*,*,#1997,.F.);
#2543=ORIENTED_EDGE('',*,*,#2003,.F.);
#2544=ORIENTED_EDGE('',*,*,#2004,.T.);
#2545=ORIENTED_EDGE('',*,*,#2005,.F.);
#2546=ORIENTED_EDGE('',*,*,#2006,.F.);
#2547=ORIENTED_EDGE('',*,*,#2007,.F.);
#2548=ORIENTED_EDGE('',*,*,#2008,.F.);
#2549=ORIENTED_EDGE('',*,*,#2009,.F.);
#2550=ORIENTED_EDGE('',*,*,#2004,.F.);
#2551=ORIENTED_EDGE('',*,*,#2010,.F.);
#2552=ORIENTED_EDGE('',*,*,#2011,.T.);
#2553=ORIENTED_EDGE('',*,*,#2012,.F.);
#2554=ORIENTED_EDGE('',*,*,#2013,.F.);
#2555=ORIENTED_EDGE('',*,*,#2014,.F.);
#2556=ORIENTED_EDGE('',*,*,#2015,.F.);
#2557=ORIENTED_EDGE('',*,*,#2016,.F.);
#2558=ORIENTED_EDGE('',*,*,#2011,.F.);
#2559=ORIENTED_EDGE('',*,*,#2017,.F.);
#2560=ORIENTED_EDGE('',*,*,#2018,.T.);
#2561=ORIENTED_EDGE('',*,*,#2019,.F.);
#2562=ORIENTED_EDGE('',*,*,#2020,.F.);
#2563=ORIENTED_EDGE('',*,*,#2021,.F.);
#2564=ORIENTED_EDGE('',*,*,#2022,.F.);
#2565=ORIENTED_EDGE('',*,*,#2023,.F.);
#2566=ORIENTED_EDGE('',*,*,#2018,.F.);
#2567=ORIENTED_EDGE('',*,*,#2024,.F.);
#2568=ORIENTED_EDGE('',*,*,#2025,.T.);
#2569=ORIENTED_EDGE('',*,*,#2026,.F.);
#2570=ORIENTED_EDGE('',*,*,#2027,.F.);
#2571=ORIENTED_EDGE('',*,*,#2028,.F.);
#2572=ORIENTED_EDGE('',*,*,#2029,.F.);
#2573=ORIENTED_EDGE('',*,*,#2030,.F.);
#2574=ORIENTED_EDGE('',*,*,#2025,.F.);
#2575=ORIENTED_EDGE('',*,*,#2031,.F.);
#2576=ORIENTED_EDGE('',*,*,#2032,.T.);
#2577=ORIENTED_EDGE('',*,*,#2033,.F.);
#2578=ORIENTED_EDGE('',*,*,#2034,.F.);
#2579=ORIENTED_EDGE('',*,*,#2035,.F.);
#2580=ORIENTED_EDGE('',*,*,#2036,.F.);
#2581=ORIENTED_EDGE('',*,*,#2037,.F.);
#2582=ORIENTED_EDGE('',*,*,#2032,.F.);
#2583=ORIENTED_EDGE('',*,*,#2038,.F.);
#2584=ORIENTED_EDGE('',*,*,#2039,.T.);
#2585=ORIENTED_EDGE('',*,*,#2040,.F.);
#2586=ORIENTED_EDGE('',*,*,#2041,.F.);
#2587=ORIENTED_EDGE('',*,*,#2042,.F.);
#2588=ORIENTED_EDGE('',*,*,#2043,.F.);
#2589=ORIENTED_EDGE('',*,*,#2044,.F.);
#2590=ORIENTED_EDGE('',*,*,#2039,.F.);
#2591=ORIENTED_EDGE('',*,*,#1978,.T.);
#2592=ORIENTED_EDGE('',*,*,#2045,.T.);
#2593=ORIENTED_EDGE('',*,*,#2034,.T.);
#2594=ORIENTED_EDGE('',*,*,#2046,.T.);
#2595=ORIENTED_EDGE('',*,*,#1986,.T.);
#2596=ORIENTED_EDGE('',*,*,#2047,.T.);
#2597=ORIENTED_EDGE('',*,*,#2028,.T.);
#2598=ORIENTED_EDGE('',*,*,#2048,.T.);
#2599=ORIENTED_EDGE('',*,*,#2021,.T.);
#2600=ORIENTED_EDGE('',*,*,#2049,.T.);
#2601=ORIENTED_EDGE('',*,*,#2001,.T.);
#2602=ORIENTED_EDGE('',*,*,#2050,.T.);
#2603=ORIENTED_EDGE('',*,*,#2015,.T.);
#2604=ORIENTED_EDGE('',*,*,#2051,.T.);
#2605=ORIENTED_EDGE('',*,*,#2008,.T.);
#2606=ORIENTED_EDGE('',*,*,#2052,.T.);
#2607=ORIENTED_EDGE('',*,*,#1991,.T.);
#2608=ORIENTED_EDGE('',*,*,#1995,.T.);
#2609=ORIENTED_EDGE('',*,*,#2053,.T.);
#2610=ORIENTED_EDGE('',*,*,#2041,.T.);
#2611=ORIENTED_EDGE('',*,*,#2054,.T.);
#2612=ORIENTED_EDGE('',*,*,#2055,.T.);
#2613=ORIENTED_EDGE('',*,*,#2022,.T.);
#2614=ORIENTED_EDGE('',*,*,#2048,.F.);
#2615=ORIENTED_EDGE('',*,*,#2027,.T.);
#2616=ORIENTED_EDGE('',*,*,#2056,.F.);
#2617=ORIENTED_EDGE('',*,*,#2005,.T.);
#2618=ORIENTED_EDGE('',*,*,#2009,.T.);
#2619=ORIENTED_EDGE('',*,*,#2051,.F.);
#2620=ORIENTED_EDGE('',*,*,#2014,.T.);
#2621=ORIENTED_EDGE('',*,*,#2057,.F.);
#2622=ORIENTED_EDGE('',*,*,#1998,.T.);
#2623=ORIENTED_EDGE('',*,*,#2002,.T.);
#2624=ORIENTED_EDGE('',*,*,#2049,.F.);
#2625=ORIENTED_EDGE('',*,*,#2020,.T.);
#2626=ORIENTED_EDGE('',*,*,#2058,.F.);
#2627=ORIENTED_EDGE('',*,*,#2000,.T.);
#2628=ORIENTED_EDGE('',*,*,#2059,.F.);
#2629=ORIENTED_EDGE('',*,*,#2012,.T.);
#2630=ORIENTED_EDGE('',*,*,#2016,.T.);
#2631=ORIENTED_EDGE('',*,*,#2050,.F.);
#2632=ORIENTED_EDGE('',*,*,#1992,.T.);
#2633=ORIENTED_EDGE('',*,*,#2052,.F.);
#2634=ORIENTED_EDGE('',*,*,#2007,.T.);
#2635=ORIENTED_EDGE('',*,*,#2060,.F.);
#2636=ORIENTED_EDGE('',*,*,#1994,.T.);
#2637=ORIENTED_EDGE('',*,*,#2061,.F.);
#2638=ORIENTED_EDGE('',*,*,#2042,.T.);
#2639=ORIENTED_EDGE('',*,*,#2053,.F.);
#2640=ORIENTED_EDGE('',*,*,#1987,.T.);
#2641=ORIENTED_EDGE('',*,*,#2046,.F.);
#2642=ORIENTED_EDGE('',*,*,#2033,.T.);
#2643=ORIENTED_EDGE('',*,*,#2037,.T.);
#2644=ORIENTED_EDGE('',*,*,#2062,.F.);
#2645=ORIENTED_EDGE('',*,*,#1985,.T.);
#2646=ORIENTED_EDGE('',*,*,#2063,.F.);
#2647=ORIENTED_EDGE('',*,*,#2029,.T.);
#2648=ORIENTED_EDGE('',*,*,#2047,.F.);
#2649=ORIENTED_EDGE('',*,*,#1979,.T.);
#2650=ORIENTED_EDGE('',*,*,#2054,.F.);
#2651=ORIENTED_EDGE('',*,*,#2040,.T.);
#2652=ORIENTED_EDGE('',*,*,#2044,.T.);
#2653=ORIENTED_EDGE('',*,*,#2064,.F.);
#2654=ORIENTED_EDGE('',*,*,#1977,.T.);
#2655=ORIENTED_EDGE('',*,*,#1981,.T.);
#2656=ORIENTED_EDGE('',*,*,#2065,.F.);
#2657=ORIENTED_EDGE('',*,*,#2035,.T.);
#2658=ORIENTED_EDGE('',*,*,#2045,.F.);
#2659=ORIENTED_EDGE('',*,*,#2066,.F.);
#2660=ORIENTED_EDGE('',*,*,#1980,.T.);
#2661=ORIENTED_EDGE('',*,*,#2064,.T.);
#2662=ORIENTED_EDGE('',*,*,#2043,.T.);
#2663=ORIENTED_EDGE('',*,*,#2061,.T.);
#2664=ORIENTED_EDGE('',*,*,#1993,.T.);
#2665=ORIENTED_EDGE('',*,*,#2060,.T.);
#2666=ORIENTED_EDGE('',*,*,#2006,.T.);
#2667=ORIENTED_EDGE('',*,*,#2057,.T.);
#2668=ORIENTED_EDGE('',*,*,#2013,.T.);
#2669=ORIENTED_EDGE('',*,*,#2059,.T.);
#2670=ORIENTED_EDGE('',*,*,#1999,.T.);
#2671=ORIENTED_EDGE('',*,*,#2058,.T.);
#2672=ORIENTED_EDGE('',*,*,#2019,.T.);
#2673=ORIENTED_EDGE('',*,*,#2023,.T.);
#2674=ORIENTED_EDGE('',*,*,#2056,.T.);
#2675=ORIENTED_EDGE('',*,*,#2026,.T.);
#2676=ORIENTED_EDGE('',*,*,#2030,.T.);
#2677=ORIENTED_EDGE('',*,*,#2063,.T.);
#2678=ORIENTED_EDGE('',*,*,#1984,.T.);
#2679=ORIENTED_EDGE('',*,*,#1988,.T.);
#2680=ORIENTED_EDGE('',*,*,#2062,.T.);
#2681=ORIENTED_EDGE('',*,*,#2036,.T.);
#2682=ORIENTED_EDGE('',*,*,#2065,.T.);
#2683=ORIENTED_EDGE('',*,*,#2067,.F.);
#2684=ORIENTED_EDGE('',*,*,#2068,.T.);
#2685=ORIENTED_EDGE('',*,*,#2066,.T.);
#2686=ORIENTED_EDGE('',*,*,#2068,.F.);
#2687=ORIENTED_EDGE('',*,*,#2067,.T.);
#2688=ORIENTED_EDGE('',*,*,#2069,.F.);
#2689=ORIENTED_EDGE('',*,*,#2038,.T.);
#2690=ORIENTED_EDGE('',*,*,#2031,.T.);
#2691=ORIENTED_EDGE('',*,*,#2024,.T.);
#2692=ORIENTED_EDGE('',*,*,#2017,.T.);
#2693=ORIENTED_EDGE('',*,*,#2010,.T.);
#2694=ORIENTED_EDGE('',*,*,#2003,.T.);
#2695=ORIENTED_EDGE('',*,*,#1996,.T.);
#2696=ORIENTED_EDGE('',*,*,#1989,.T.);
#2697=ORIENTED_EDGE('',*,*,#1982,.T.);
#2698=ORIENTED_EDGE('',*,*,#1975,.T.);
#2699=ORIENTED_EDGE('',*,*,#2069,.T.);
#2700=ORIENTED_EDGE('',*,*,#2070,.T.);
#2701=ORIENTED_EDGE('',*,*,#2055,.F.);
#2702=ORIENTED_EDGE('',*,*,#2070,.F.);
#3436=CYLINDRICAL_SURFACE('',#4006,0.22);
#3437=CYLINDRICAL_SURFACE('',#4010,0.22);
#3438=CYLINDRICAL_SURFACE('',#4015,0.22);
#3439=CYLINDRICAL_SURFACE('',#4020,0.22);
#3440=CYLINDRICAL_SURFACE('',#4024,0.22);
#3441=CYLINDRICAL_SURFACE('',#4028,0.22);
#3442=CYLINDRICAL_SURFACE('',#4032,0.22);
#3443=CYLINDRICAL_SURFACE('',#4037,0.22);
#3444=CYLINDRICAL_SURFACE('',#4042,0.22);
#3445=CYLINDRICAL_SURFACE('',#4046,0.22);
#3446=CYLINDRICAL_SURFACE('',#4084,1.4);
#3447=CYLINDRICAL_SURFACE('',#4088,0.75);
#3515=ADVANCED_FACE('',(#544),#3436,.F.);
#3516=ADVANCED_FACE('',(#545),#3437,.F.);
#3517=ADVANCED_FACE('',(#546),#3438,.F.);
#3518=ADVANCED_FACE('',(#547),#3439,.F.);
#3519=ADVANCED_FACE('',(#548),#3440,.F.);
#3520=ADVANCED_FACE('',(#549),#3441,.F.);
#3521=ADVANCED_FACE('',(#550),#3442,.F.);
#3522=ADVANCED_FACE('',(#551),#3443,.F.);
#3523=ADVANCED_FACE('',(#552),#3444,.F.);
#3524=ADVANCED_FACE('',(#553),#3445,.F.);
#3525=ADVANCED_FACE('',(#554,#382),#449,.T.);
#3526=ADVANCED_FACE('',(#555),#170,.F.);
#3527=ADVANCED_FACE('',(#556),#171,.F.);
#3528=ADVANCED_FACE('',(#557),#172,.F.);
#3529=ADVANCED_FACE('',(#558),#173,.F.);
#3530=ADVANCED_FACE('',(#559),#174,.F.);
#3531=ADVANCED_FACE('',(#560),#175,.F.);
#3532=ADVANCED_FACE('',(#561),#176,.F.);
#3533=ADVANCED_FACE('',(#562),#177,.F.);
#3534=ADVANCED_FACE('',(#563),#178,.F.);
#3535=ADVANCED_FACE('',(#564),#179,.F.);
#3536=ADVANCED_FACE('',(#565,#383),#450,.T.);
#3537=ADVANCED_FACE('',(#566),#3446,.T.);
#3538=ADVANCED_FACE('',(#567,#384,#385,#386,#387,#388,#389,#390,#391,#392,
#393,#394),#451,.T.);
#3539=ADVANCED_FACE('',(#568),#3447,.F.);
#3706=CLOSED_SHELL('',(#3515,#3516,#3517,#3518,#3519,#3520,#3521,#3522,
#3523,#3524,#3525,#3526,#3527,#3528,#3529,#3530,#3531,#3532,#3533,#3534,
#3535,#3536,#3537,#3538,#3539));
#4005=AXIS2_PLACEMENT_3D('',#5788,#4596,#4597);
#4006=AXIS2_PLACEMENT_3D('',#5789,#4598,#4599);
#4007=AXIS2_PLACEMENT_3D('',#5791,#4600,#4601);
#4008=AXIS2_PLACEMENT_3D('',#5806,#4603,#4604);
#4009=AXIS2_PLACEMENT_3D('',#5825,#4605,#4606);
#4010=AXIS2_PLACEMENT_3D('',#5836,#4607,#4608);
#4011=AXIS2_PLACEMENT_3D('',#5838,#4609,#4610);
#4012=AXIS2_PLACEMENT_3D('',#5842,#4612,#4613);
#4013=AXIS2_PLACEMENT_3D('',#5861,#4614,#4615);
#4014=AXIS2_PLACEMENT_3D('',#5879,#4616,#4617);
#4015=AXIS2_PLACEMENT_3D('',#5880,#4618,#4619);
#4016=AXIS2_PLACEMENT_3D('',#5882,#4620,#4621);
#4017=AXIS2_PLACEMENT_3D('',#5886,#4623,#4624);
#4018=AXIS2_PLACEMENT_3D('',#5905,#4625,#4626);
#4019=AXIS2_PLACEMENT_3D('',#5923,#4627,#4628);
#4020=AXIS2_PLACEMENT_3D('',#5924,#4629,#4630);
#4021=AXIS2_PLACEMENT_3D('',#5926,#4631,#4632);
#4022=AXIS2_PLACEMENT_3D('',#5939,#4634,#4635);
#4023=AXIS2_PLACEMENT_3D('',#5958,#4636,#4637);
#4024=AXIS2_PLACEMENT_3D('',#5971,#4638,#4639);
#4025=AXIS2_PLACEMENT_3D('',#5973,#4640,#4641);
#4026=AXIS2_PLACEMENT_3D('',#5994,#4643,#4644);
#4027=AXIS2_PLACEMENT_3D('',#6013,#4645,#4646);
#4028=AXIS2_PLACEMENT_3D('',#6018,#4647,#4648);
#4029=AXIS2_PLACEMENT_3D('',#6020,#4649,#4650);
#4030=AXIS2_PLACEMENT_3D('',#6037,#4652,#4653);
#4031=AXIS2_PLACEMENT_3D('',#6056,#4654,#4655);
#4032=AXIS2_PLACEMENT_3D('',#6065,#4656,#4657);
#4033=AXIS2_PLACEMENT_3D('',#6067,#4658,#4659);
#4034=AXIS2_PLACEMENT_3D('',#6071,#4661,#4662);
#4035=AXIS2_PLACEMENT_3D('',#6090,#4663,#4664);
#4036=AXIS2_PLACEMENT_3D('',#6108,#4665,#4666);
#4037=AXIS2_PLACEMENT_3D('',#6109,#4667,#4668);
#4038=AXIS2_PLACEMENT_3D('',#6111,#4669,#4670);
#4039=AXIS2_PLACEMENT_3D('',#6115,#4672,#4673);
#4040=AXIS2_PLACEMENT_3D('',#6134,#4674,#4675);
#4041=AXIS2_PLACEMENT_3D('',#6152,#4676,#4677);
#4042=AXIS2_PLACEMENT_3D('',#6153,#4678,#4679);
#4043=AXIS2_PLACEMENT_3D('',#6155,#4680,#4681);
#4044=AXIS2_PLACEMENT_3D('',#6174,#4683,#4684);
#4045=AXIS2_PLACEMENT_3D('',#6193,#4685,#4686);
#4046=AXIS2_PLACEMENT_3D('',#6200,#4687,#4688);
#4047=AXIS2_PLACEMENT_3D('',#6202,#4689,#4690);
#4048=AXIS2_PLACEMENT_3D('',#6211,#4692,#4693);
#4049=AXIS2_PLACEMENT_3D('',#6230,#4694,#4695);
#4050=AXIS2_PLACEMENT_3D('',#6247,#4696,#4697);
#4051=AXIS2_PLACEMENT_3D('',#6248,#4698,#4699);
#4052=AXIS2_PLACEMENT_3D('',#6249,#4700,#4701);
#4053=AXIS2_PLACEMENT_3D('',#6250,#4702,#4703);
#4054=AXIS2_PLACEMENT_3D('',#6251,#4704,#4705);
#4055=AXIS2_PLACEMENT_3D('',#6252,#4706,#4707);
#4056=AXIS2_PLACEMENT_3D('',#6253,#4708,#4709);
#4057=AXIS2_PLACEMENT_3D('',#6254,#4710,#4711);
#4058=AXIS2_PLACEMENT_3D('',#6255,#4712,#4713);
#4059=AXIS2_PLACEMENT_3D('',#6256,#4714,#4715);
#4060=AXIS2_PLACEMENT_3D('',#6257,#4716,#4717);
#4061=AXIS2_PLACEMENT_3D('',#6259,#4718,#4719);
#4062=AXIS2_PLACEMENT_3D('',#6260,#4720,#4721);
#4063=AXIS2_PLACEMENT_3D('',#6261,#4722,#4723);
#4064=AXIS2_PLACEMENT_3D('',#6262,#4724,#4725);
#4065=AXIS2_PLACEMENT_3D('',#6263,#4726,#4727);
#4066=AXIS2_PLACEMENT_3D('',#6264,#4728,#4729);
#4067=AXIS2_PLACEMENT_3D('',#6265,#4730,#4731);
#4068=AXIS2_PLACEMENT_3D('',#6266,#4732,#4733);
#4069=AXIS2_PLACEMENT_3D('',#6267,#4734,#4735);
#4070=AXIS2_PLACEMENT_3D('',#6268,#4736,#4737);
#4071=AXIS2_PLACEMENT_3D('',#6269,#4738,#4739);
#4072=AXIS2_PLACEMENT_3D('',#6270,#4740,#4741);
#4073=AXIS2_PLACEMENT_3D('',#6271,#4742,#4743);
#4074=AXIS2_PLACEMENT_3D('',#6272,#4744,#4745);
#4075=AXIS2_PLACEMENT_3D('',#6273,#4746,#4747);
#4076=AXIS2_PLACEMENT_3D('',#6274,#4748,#4749);
#4077=AXIS2_PLACEMENT_3D('',#6275,#4750,#4751);
#4078=AXIS2_PLACEMENT_3D('',#6276,#4752,#4753);
#4079=AXIS2_PLACEMENT_3D('',#6277,#4754,#4755);
#4080=AXIS2_PLACEMENT_3D('',#6278,#4756,#4757);
#4081=AXIS2_PLACEMENT_3D('',#6279,#4758,#4759);
#4082=AXIS2_PLACEMENT_3D('',#6280,#4760,#4761);
#4083=AXIS2_PLACEMENT_3D('',#6282,#4762,#4763);
#4084=AXIS2_PLACEMENT_3D('',#6283,#4764,#4765);
#4085=AXIS2_PLACEMENT_3D('',#6285,#4766,#4767);
#4086=AXIS2_PLACEMENT_3D('',#6287,#4769,#4770);
#4087=AXIS2_PLACEMENT_3D('',#6289,#4771,#4772);
#4088=AXIS2_PLACEMENT_3D('',#6290,#4773,#4774);
#4596=DIRECTION('axis',(0.,0.,1.));
#4597=DIRECTION('refdir',(1.,0.,0.));
#4598=DIRECTION('center_axis',(0.,1.,0.));
#4599=DIRECTION('ref_axis',(1.,0.,0.));
#4600=DIRECTION('center_axis',(0.,1.,0.));
#4601=DIRECTION('ref_axis',(1.,0.,0.));
#4602=DIRECTION('',(0.,1.,0.));
#4603=DIRECTION('center_axis',(0.,-1.,0.));
#4604=DIRECTION('ref_axis',(1.,0.,0.));
#4605=DIRECTION('center_axis',(0.,-1.,0.));
#4606=DIRECTION('ref_axis',(1.,0.,0.));
#4607=DIRECTION('center_axis',(0.,1.,0.));
#4608=DIRECTION('ref_axis',(1.,0.,0.));
#4609=DIRECTION('center_axis',(0.,1.,0.));
#4610=DIRECTION('ref_axis',(1.,0.,0.));
#4611=DIRECTION('',(0.,1.,0.));
#4612=DIRECTION('center_axis',(0.,-1.,0.));
#4613=DIRECTION('ref_axis',(1.,0.,0.));
#4614=DIRECTION('center_axis',(0.,-1.,0.));
#4615=DIRECTION('ref_axis',(1.,0.,0.));
#4616=DIRECTION('center_axis',(0.,-1.,0.));
#4617=DIRECTION('ref_axis',(1.,0.,0.));
#4618=DIRECTION('center_axis',(0.,1.,0.));
#4619=DIRECTION('ref_axis',(1.,0.,0.));
#4620=DIRECTION('center_axis',(0.,1.,0.));
#4621=DIRECTION('ref_axis',(1.,0.,0.));
#4622=DIRECTION('',(0.,1.,0.));
#4623=DIRECTION('center_axis',(0.,-1.,0.));
#4624=DIRECTION('ref_axis',(1.,0.,0.));
#4625=DIRECTION('center_axis',(0.,-1.,0.));
#4626=DIRECTION('ref_axis',(1.,0.,0.));
#4627=DIRECTION('center_axis',(0.,-1.,0.));
#4628=DIRECTION('ref_axis',(1.,0.,0.));
#4629=DIRECTION('center_axis',(0.,1.,0.));
#4630=DIRECTION('ref_axis',(1.,0.,0.));
#4631=DIRECTION('center_axis',(0.,1.,0.));
#4632=DIRECTION('ref_axis',(1.,0.,0.));
#4633=DIRECTION('',(0.,1.,0.));
#4634=DIRECTION('center_axis',(0.,-1.,0.));
#4635=DIRECTION('ref_axis',(1.,0.,0.));
#4636=DIRECTION('center_axis',(0.,-1.,0.));
#4637=DIRECTION('ref_axis',(1.,0.,0.));
#4638=DIRECTION('center_axis',(0.,1.,0.));
#4639=DIRECTION('ref_axis',(1.,0.,0.));
#4640=DIRECTION('center_axis',(0.,1.,0.));
#4641=DIRECTION('ref_axis',(1.,0.,0.));
#4642=DIRECTION('',(0.,1.,0.));
#4643=DIRECTION('center_axis',(0.,-1.,0.));
#4644=DIRECTION('ref_axis',(1.,0.,0.));
#4645=DIRECTION('center_axis',(0.,-1.,0.));
#4646=DIRECTION('ref_axis',(1.,0.,0.));
#4647=DIRECTION('center_axis',(0.,1.,0.));
#4648=DIRECTION('ref_axis',(1.,0.,0.));
#4649=DIRECTION('center_axis',(0.,1.,0.));
#4650=DIRECTION('ref_axis',(1.,0.,0.));
#4651=DIRECTION('',(0.,1.,0.));
#4652=DIRECTION('center_axis',(0.,-1.,0.));
#4653=DIRECTION('ref_axis',(1.,0.,0.));
#4654=DIRECTION('center_axis',(0.,-1.,0.));
#4655=DIRECTION('ref_axis',(1.,0.,0.));
#4656=DIRECTION('center_axis',(0.,1.,0.));
#4657=DIRECTION('ref_axis',(1.,0.,0.));
#4658=DIRECTION('center_axis',(0.,1.,0.));
#4659=DIRECTION('ref_axis',(1.,0.,0.));
#4660=DIRECTION('',(0.,1.,0.));
#4661=DIRECTION('center_axis',(0.,-1.,0.));
#4662=DIRECTION('ref_axis',(1.,0.,0.));
#4663=DIRECTION('center_axis',(0.,-1.,0.));
#4664=DIRECTION('ref_axis',(1.,0.,0.));
#4665=DIRECTION('center_axis',(0.,-1.,0.));
#4666=DIRECTION('ref_axis',(1.,0.,0.));
#4667=DIRECTION('center_axis',(0.,1.,0.));
#4668=DIRECTION('ref_axis',(1.,0.,0.));
#4669=DIRECTION('center_axis',(0.,1.,0.));
#4670=DIRECTION('ref_axis',(1.,0.,0.));
#4671=DIRECTION('',(0.,1.,0.));
#4672=DIRECTION('center_axis',(0.,-1.,0.));
#4673=DIRECTION('ref_axis',(1.,0.,0.));
#4674=DIRECTION('center_axis',(0.,-1.,0.));
#4675=DIRECTION('ref_axis',(1.,0.,0.));
#4676=DIRECTION('center_axis',(0.,-1.,0.));
#4677=DIRECTION('ref_axis',(1.,0.,0.));
#4678=DIRECTION('center_axis',(0.,1.,0.));
#4679=DIRECTION('ref_axis',(1.,0.,0.));
#4680=DIRECTION('center_axis',(0.,1.,0.));
#4681=DIRECTION('ref_axis',(1.,0.,0.));
#4682=DIRECTION('',(0.,1.,0.));
#4683=DIRECTION('center_axis',(0.,-1.,0.));
#4684=DIRECTION('ref_axis',(1.,0.,0.));
#4685=DIRECTION('center_axis',(0.,-1.,0.));
#4686=DIRECTION('ref_axis',(1.,0.,0.));
#4687=DIRECTION('center_axis',(0.,1.,0.));
#4688=DIRECTION('ref_axis',(1.,0.,0.));
#4689=DIRECTION('center_axis',(0.,1.,0.));
#4690=DIRECTION('ref_axis',(1.,0.,0.));
#4691=DIRECTION('',(0.,1.,0.));
#4692=DIRECTION('center_axis',(0.,-1.,0.));
#4693=DIRECTION('ref_axis',(1.,0.,0.));
#4694=DIRECTION('center_axis',(0.,-1.,0.));
#4695=DIRECTION('ref_axis',(1.,0.,0.));
#4696=DIRECTION('center_axis',(0.,1.,0.));
#4697=DIRECTION('ref_axis',(0.,0.,1.));
#4698=DIRECTION('center_axis',(0.,1.,0.));
#4699=DIRECTION('ref_axis',(0.,0.,-1.));
#4700=DIRECTION('center_axis',(0.,1.,0.));
#4701=DIRECTION('ref_axis',(0.,0.,-1.));
#4702=DIRECTION('center_axis',(0.,1.,0.));
#4703=DIRECTION('ref_axis',(0.,0.,-1.));
#4704=DIRECTION('center_axis',(0.,1.,0.));
#4705=DIRECTION('ref_axis',(0.,0.,-1.));
#4706=DIRECTION('center_axis',(0.,1.,0.));
#4707=DIRECTION('ref_axis',(0.,0.,-1.));
#4708=DIRECTION('center_axis',(0.,1.,0.));
#4709=DIRECTION('ref_axis',(0.,0.,-1.));
#4710=DIRECTION('center_axis',(0.,1.,0.));
#4711=DIRECTION('ref_axis',(0.,0.,-1.));
#4712=DIRECTION('center_axis',(0.,1.,0.));
#4713=DIRECTION('ref_axis',(0.,0.,-1.));
#4714=DIRECTION('center_axis',(0.,1.,0.));
#4715=DIRECTION('ref_axis',(0.,0.,-1.));
#4716=DIRECTION('center_axis',(0.,1.,0.));
#4717=DIRECTION('ref_axis',(0.,0.,-1.));
#4718=DIRECTION('center_axis',(0.,-1.,0.));
#4719=DIRECTION('ref_axis',(1.,0.,0.));
#4720=DIRECTION('center_axis',(0.,-1.,0.));
#4721=DIRECTION('ref_axis',(0.,0.,-1.));
#4722=DIRECTION('center_axis',(0.,-1.,0.));
#4723=DIRECTION('ref_axis',(0.,0.,-1.));
#4724=DIRECTION('center_axis',(0.,-1.,0.));
#4725=DIRECTION('ref_axis',(0.,0.,-1.));
#4726=DIRECTION('center_axis',(0.,-1.,0.));
#4727=DIRECTION('ref_axis',(0.,0.,-1.));
#4728=DIRECTION('center_axis',(0.,-1.,0.));
#4729=DIRECTION('ref_axis',(0.,0.,-1.));
#4730=DIRECTION('center_axis',(0.,-1.,0.));
#4731=DIRECTION('ref_axis',(0.,0.,-1.));
#4732=DIRECTION('center_axis',(0.,-1.,0.));
#4733=DIRECTION('ref_axis',(-1.22464679914735E-16,0.,1.));
#4734=DIRECTION('center_axis',(0.,-1.,0.));
#4735=DIRECTION('ref_axis',(0.,0.,-1.));
#4736=DIRECTION('center_axis',(0.,-1.,0.));
#4737=DIRECTION('ref_axis',(0.,0.,-1.));
#4738=DIRECTION('center_axis',(0.,-1.,0.));
#4739=DIRECTION('ref_axis',(0.,0.,-1.));
#4740=DIRECTION('center_axis',(0.,-1.,0.));
#4741=DIRECTION('ref_axis',(0.,0.,-1.));
#4742=DIRECTION('center_axis',(0.,-1.,0.));
#4743=DIRECTION('ref_axis',(0.,0.,-1.));
#4744=DIRECTION('center_axis',(0.,-1.,0.));
#4745=DIRECTION('ref_axis',(0.,0.,-1.));
#4746=DIRECTION('center_axis',(0.,-1.,0.));
#4747=DIRECTION('ref_axis',(0.,0.,-1.));
#4748=DIRECTION('center_axis',(0.,-1.,0.));
#4749=DIRECTION('ref_axis',(0.,0.,-1.));
#4750=DIRECTION('center_axis',(0.,-1.,0.));
#4751=DIRECTION('ref_axis',(0.,0.,-1.));
#4752=DIRECTION('center_axis',(0.,-1.,0.));
#4753=DIRECTION('ref_axis',(0.,0.,-1.));
#4754=DIRECTION('center_axis',(0.,-1.,0.));
#4755=DIRECTION('ref_axis',(0.,0.,-1.));
#4756=DIRECTION('center_axis',(0.,-1.,0.));
#4757=DIRECTION('ref_axis',(0.,0.,-1.));
#4758=DIRECTION('center_axis',(0.,-1.,0.));
#4759=DIRECTION('ref_axis',(0.,0.,-1.));
#4760=DIRECTION('center_axis',(0.,1.,0.));
#4761=DIRECTION('ref_axis',(0.,0.,1.));
#4762=DIRECTION('center_axis',(0.,-1.,0.));
#4763=DIRECTION('ref_axis',(1.,0.,0.));
#4764=DIRECTION('center_axis',(0.,-1.,0.));
#4765=DIRECTION('ref_axis',(1.,0.,0.));
#4766=DIRECTION('center_axis',(0.,-1.,0.));
#4767=DIRECTION('ref_axis',(1.,0.,0.));
#4768=DIRECTION('',(0.,1.,0.));
#4769=DIRECTION('center_axis',(0.,-1.,0.));
#4770=DIRECTION('ref_axis',(0.,0.,-1.));
#4771=DIRECTION('center_axis',(0.,-1.,0.));
#4772=DIRECTION('ref_axis',(1.,0.,0.));
#4773=DIRECTION('center_axis',(0.,-1.,0.));
#4774=DIRECTION('ref_axis',(1.,0.,0.));
#4775=DIRECTION('',(0.,1.,0.));
#5788=CARTESIAN_POINT('',(0.,0.,0.));
#5789=CARTESIAN_POINT('Origin',(0.339918693812442,0.,-1.04616216792467));
#5790=CARTESIAN_POINT('',(0.119918693812442,0.,-1.04616216792467));
#5791=CARTESIAN_POINT('Origin',(0.339918693812442,0.,-1.04616216792467));
#5792=CARTESIAN_POINT('',(0.119918693812442,0.247376716776579,-1.04616216792467));
#5793=CARTESIAN_POINT('',(0.119918693812442,0.,-1.04616216792467));
#5794=CARTESIAN_POINT('',(0.174765758038764,0.35,-0.900819442598166));
#5795=CARTESIAN_POINT('Ctrl Pts',(0.174765758038763,0.35,-0.900819442598166));
#5796=CARTESIAN_POINT('Ctrl Pts',(0.16615910126156,0.335479408675346,-0.910599186515576));
#5797=CARTESIAN_POINT('Ctrl Pts',(0.157611943697822,0.321649098925924,-0.922105787154342));
#5798=CARTESIAN_POINT('Ctrl Pts',(0.142410854924046,0.296417377297428,-0.948090475176036));
#5799=CARTESIAN_POINT('Ctrl Pts',(0.135635598256597,0.284856881183445,-0.962749516762522));
#5800=CARTESIAN_POINT('Ctrl Pts',(0.124807600924644,0.264292426692751,-0.996493855518017));
#5801=CARTESIAN_POINT('Ctrl Pts',(0.12107905659851,0.255687624123886,-1.01568738120414));
#5802=CARTESIAN_POINT('Ctrl Pts',(0.119995150322276,0.24900173289775,-1.03947451044843));
#5803=CARTESIAN_POINT('Ctrl Pts',(0.119918693812442,0.248148180937244,-1.04281359823645));
#5804=CARTESIAN_POINT('Ctrl Pts',(0.119918693812442,0.247376716776579,-1.04616216792467));
#5805=CARTESIAN_POINT('',(0.388099915049348,0.35,-0.831502973106184));
#5806=CARTESIAN_POINT('Origin',(0.339918693812442,0.35,-1.04616216792467));
#5807=CARTESIAN_POINT('',(0.52031818912536,0.35,-1.17208286555157));
#5808=CARTESIAN_POINT('Ctrl Pts',(0.52031818912536,0.35,-1.17208286555157));
#5809=CARTESIAN_POINT('Ctrl Pts',(0.529217457694123,0.335332571878444,-1.15933338442007));
#5810=CARTESIAN_POINT('Ctrl Pts',(0.537396458457103,0.321517770338583,-1.14467059284705));
#5811=CARTESIAN_POINT('Ctrl Pts',(0.550248212225112,0.296532793702566,-1.11286085586034));
#5812=CARTESIAN_POINT('Ctrl Pts',(0.555078018641098,0.285216775966753,-1.09565550010774));
#5813=CARTESIAN_POINT('Ctrl Pts',(0.560591549482129,0.264680669899339,-1.05711602071761));
#5814=CARTESIAN_POINT('Ctrl Pts',(0.56078880978987,0.255831783241444,-1.03561092919333));
#5815=CARTESIAN_POINT('Ctrl Pts',(0.554627960771623,0.244745328150165,-0.994433608378458));
#5816=CARTESIAN_POINT('Ctrl Pts',(0.549175023311742,0.241941375180247,-0.975354466173215));
#5817=CARTESIAN_POINT('Ctrl Pts',(0.532711855060331,0.242062069598183,-0.938206075044727));
#5818=CARTESIAN_POINT('Ctrl Pts',(0.521946739366384,0.245143826724661,-0.921041750757787));
#5819=CARTESIAN_POINT('Ctrl Pts',(0.494476822014916,0.25808943656053,-0.887869891643464));
#5820=CARTESIAN_POINT('Ctrl Pts',(0.477731860324512,0.268767859044401,-0.873445791067852));
#5821=CARTESIAN_POINT('Ctrl Pts',(0.43505445349855,0.301421636034264,-0.84547220309525));
#5822=CARTESIAN_POINT('Ctrl Pts',(0.409474560891576,0.32558298615786,-0.836300608451158));
#5823=CARTESIAN_POINT('Ctrl Pts',(0.388099915049348,0.35,-0.831502973106184));
#5824=CARTESIAN_POINT('',(0.267986765351098,0.35,-1.25407031511432));
#5825=CARTESIAN_POINT('Origin',(0.339918693812442,0.35,-1.04616216792467));
#5826=CARTESIAN_POINT('Ctrl Pts',(0.119918693812442,0.247376716776579,-1.04616216792467));
#5827=CARTESIAN_POINT('Ctrl Pts',(0.119918693812442,0.243706481856949,-1.0620929629339));
#5828=CARTESIAN_POINT('Ctrl Pts',(0.121649354618456,0.241892736284291,-1.07823803146977));
#5829=CARTESIAN_POINT('Ctrl Pts',(0.129925208402574,0.242150819014083,-1.11515786183808));
#5830=CARTESIAN_POINT('Ctrl Pts',(0.137545730009388,0.245541115579871,-1.13486353269143));
#5831=CARTESIAN_POINT('Ctrl Pts',(0.159894075495139,0.25896926022056,-1.17516872094799));
#5832=CARTESIAN_POINT('Ctrl Pts',(0.175488151194729,0.270150443771654,-1.19412647612185));
#5833=CARTESIAN_POINT('Ctrl Pts',(0.216960528286492,0.30273418323525,-1.2315190249125));
#5834=CARTESIAN_POINT('Ctrl Pts',(0.243776713476771,0.325833097600423,-1.24569413677302));
#5835=CARTESIAN_POINT('Ctrl Pts',(0.267986765351098,0.35,-1.25407031511432));
#5836=CARTESIAN_POINT('Origin',(-0.889918693812442,0.,-0.64656377752172));
#5837=CARTESIAN_POINT('',(-1.10991869381244,0.,-0.64656377752172));
#5838=CARTESIAN_POINT('Origin',(-0.889918693812442,0.,-0.64656377752172));
#5839=CARTESIAN_POINT('',(-1.10991869381244,0.35,-0.64656377752172));
#5840=CARTESIAN_POINT('',(-1.10991869381244,0.,-0.64656377752172));
#5841=CARTESIAN_POINT('',(-1.10987928032073,0.35,-0.642399598979491));
#5842=CARTESIAN_POINT('Origin',(-0.889918693812442,0.35,-0.64656377752172));
#5843=CARTESIAN_POINT('',(-0.802724611619556,0.35,-0.444580629634229));
#5844=CARTESIAN_POINT('Ctrl Pts',(-0.802724611619556,0.35,-0.444580629634229));
#5845=CARTESIAN_POINT('Ctrl Pts',(-0.814693298418458,0.335469703254327,
-0.439413868588076));
#5846=CARTESIAN_POINT('Ctrl Pts',(-0.828288194978147,0.321630486900879,
-0.43483810386629));
#5847=CARTESIAN_POINT('Ctrl Pts',(-0.857626293279467,0.296466623645907,
-0.42843076421223));
#5848=CARTESIAN_POINT('Ctrl Pts',(-0.873562500583475,0.284968850954313,
-0.426522755127025));
#5849=CARTESIAN_POINT('Ctrl Pts',(-0.908944175205009,0.264389371081104,
-0.426610046318699));
#5850=CARTESIAN_POINT('Ctrl Pts',(-0.92841189425645,0.255739222721824,-0.428985062409478));
#5851=CARTESIAN_POINT('Ctrl Pts',(-0.966701070362238,0.244572490203357,
-0.439509162402781));
#5852=CARTESIAN_POINT('Ctrl Pts',(-0.984800606765884,0.24187970665778,-0.447081989738821));
#5853=CARTESIAN_POINT('Ctrl Pts',(-1.02033222655978,0.242137933247099,-0.468098181585364));
#5854=CARTESIAN_POINT('Ctrl Pts',(-1.03672671564999,0.245516880218307,-0.48142671327546));
#5855=CARTESIAN_POINT('Ctrl Pts',(-1.0681914718434,0.258930838869848,-0.515141616697553));
#5856=CARTESIAN_POINT('Ctrl Pts',(-1.08142350523446,0.270117119131826,-0.535848665318461));
#5857=CARTESIAN_POINT('Ctrl Pts',(-1.10419503710794,0.302714929726701,-0.586877157140458));
#5858=CARTESIAN_POINT('Ctrl Pts',(-1.10939416747485,0.325822565838319,-0.616774927746324));
#5859=CARTESIAN_POINT('Ctrl Pts',(-1.10987928032073,0.35,-0.642399598979491));
#5860=CARTESIAN_POINT('',(-0.670876851625708,0.35,-0.626053502744384));
#5861=CARTESIAN_POINT('Origin',(-0.889918693812442,0.35,-0.64656377752172));
#5862=CARTESIAN_POINT('',(-0.953929883998579,0.35,-0.857045528585688));
#5863=CARTESIAN_POINT('Ctrl Pts',(-0.95392988399858,0.35,-0.857045528585688));
#5864=CARTESIAN_POINT('Ctrl Pts',(-0.939113614143974,0.335390975831829,
-0.861551415973636));
#5865=CARTESIAN_POINT('Ctrl Pts',(-0.922713318211477,0.32162844535795,-0.864791301338213));
#5866=CARTESIAN_POINT('Ctrl Pts',(-0.888689691679126,0.296761201350329,
-0.867202773669637));
#5867=CARTESIAN_POINT('Ctrl Pts',(-0.870968703349679,0.285505993520706,
-0.866515344265356));
#5868=CARTESIAN_POINT('Ctrl Pts',(-0.832657955828336,0.264913063744833,
-0.859966994580057));
#5869=CARTESIAN_POINT('Ctrl Pts',(-0.812042610895507,0.255983013500831,
-0.853529132681505));
#5870=CARTESIAN_POINT('Ctrl Pts',(-0.774637004578397,0.244799211872409,
-0.834944631013121));
#5871=CARTESIAN_POINT('Ctrl Pts',(-0.758129671802899,0.241962745238242,
-0.823863745365518));
#5872=CARTESIAN_POINT('Ctrl Pts',(-0.72783201892456,0.242038904448235,-0.796734896229851));
#5873=CARTESIAN_POINT('Ctrl Pts',(-0.714819045120535,0.245095813663096,
-0.781209421868766));
#5874=CARTESIAN_POINT('Ctrl Pts',(-0.691707150272296,0.257996207173294,
-0.744838566725142));
#5875=CARTESIAN_POINT('Ctrl Pts',(-0.683135660593065,0.268662345405233,
-0.72444259762104));
#5876=CARTESIAN_POINT('Ctrl Pts',(-0.66965672580744,0.301328368152827,-0.675132080669759));
#5877=CARTESIAN_POINT('Ctrl Pts',(-0.668830436944159,0.325533869830935,
-0.647908424074828));
#5878=CARTESIAN_POINT('Ctrl Pts',(-0.670876851625708,0.35,-0.626053502744384));
#5879=CARTESIAN_POINT('Origin',(-0.889918693812442,0.35,-0.64656377752172));
#5880=CARTESIAN_POINT('Origin',(1.1,0.,0.));
#5881=CARTESIAN_POINT('',(0.88,0.,2.69422295812418E-17));
#5882=CARTESIAN_POINT('Origin',(1.1,0.,0.));
#5883=CARTESIAN_POINT('',(0.88,0.35,2.69422295812418E-17));
#5884=CARTESIAN_POINT('',(0.88,0.,2.69422295812418E-17));
#5885=CARTESIAN_POINT('',(0.910735790157152,0.35,0.112156403618172));
#5886=CARTESIAN_POINT('Origin',(1.1,0.35,0.));
#5887=CARTESIAN_POINT('',(1.27550420984285,0.35,0.132658480043447));
#5888=CARTESIAN_POINT('Ctrl Pts',(1.27550420984285,0.35,0.132658480043447));
#5889=CARTESIAN_POINT('Ctrl Pts',(1.26611782177473,0.33531546276274,0.145076462072449));
#5890=CARTESIAN_POINT('Ctrl Pts',(1.25468431627751,0.321485352158938,0.157400492027332));
#5891=CARTESIAN_POINT('Ctrl Pts',(1.22835219222699,0.296466041103173,0.179483010322184));
#5892=CARTESIAN_POINT('Ctrl Pts',(1.21344338101808,0.285132356747975,0.189407731207313));
#5893=CARTESIAN_POINT('Ctrl Pts',(1.17846267135551,0.264612821304931,0.206540975098488));
#5894=CARTESIAN_POINT('Ctrl Pts',(1.15809147022147,0.255787504332734,0.213351934557227));
#5895=CARTESIAN_POINT('Ctrl Pts',(1.11706033563968,0.24472949208419,0.220191916744402));
#5896=CARTESIAN_POINT('Ctrl Pts',(1.09724086630217,0.241935102766417,0.220893276198431));
#5897=CARTESIAN_POINT('Ctrl Pts',(1.05683477389847,0.242068991386358,0.216703862540943));
#5898=CARTESIAN_POINT('Ctrl Pts',(1.03718465931368,0.245158125533072,0.211762979306542));
#5899=CARTESIAN_POINT('Ctrl Pts',(0.997159417898573,0.258117110209497,0.195877882014933));
#5900=CARTESIAN_POINT('Ctrl Pts',(0.97827589203717,0.268799087403244,0.184408191234792));
#5901=CARTESIAN_POINT('Ctrl Pts',(0.938511832204562,0.301449132027476,0.1524716629431));
#5902=CARTESIAN_POINT('Ctrl Pts',(0.921897120244161,0.325597462144779,0.130991175878744));
#5903=CARTESIAN_POINT('Ctrl Pts',(0.910735790157152,0.35,0.112156403618172));
#5904=CARTESIAN_POINT('',(1.27550420984285,0.35,-0.132658480043447));
#5905=CARTESIAN_POINT('Origin',(1.1,0.35,0.));
#5906=CARTESIAN_POINT('',(0.910735790157152,0.35,-0.112156403618172));
#5907=CARTESIAN_POINT('Ctrl Pts',(0.910735790157152,0.35,-0.112156403618172));
#5908=CARTESIAN_POINT('Ctrl Pts',(0.917376089752458,0.335482002504965,-0.123361925688084));
#5909=CARTESIAN_POINT('Ctrl Pts',(0.925676503375737,0.321654073155954,-0.135044303040797));
#5910=CARTESIAN_POINT('Ctrl Pts',(0.945705763566752,0.296402587659025,-0.157548233557298));
#5911=CARTESIAN_POINT('Ctrl Pts',(0.957575956315956,0.284823988089694,-0.168539952403236));
#5912=CARTESIAN_POINT('Ctrl Pts',(0.986343324120607,0.264264067609,-0.189265250815529));
#5913=CARTESIAN_POINT('Ctrl Pts',(1.00343254919411,0.255672471019212,-0.198729556237649));
#5914=CARTESIAN_POINT('Ctrl Pts',(1.04053658704398,0.24454764112274,-0.212677811623889));
#5915=CARTESIAN_POINT('Ctrl Pts',(1.05964780090184,0.241866044436253,-0.217181471497843));
#5916=CARTESIAN_POINT('Ctrl Pts',(1.1007627783985,0.242154653351498,-0.221036398352684));
#5917=CARTESIAN_POINT('Ctrl Pts',(1.12185832284616,0.24554830260434,-0.219874810080965));
#5918=CARTESIAN_POINT('Ctrl Pts',(1.16708666484378,0.258980602991006,-0.211069922924208));
#5919=CARTESIAN_POINT('Ctrl Pts',(1.18992721371268,0.270160239182283,-0.202098025620398));
#5920=CARTESIAN_POINT('Ctrl Pts',(1.23829403807689,0.302739787597863,-0.17421352400312));
#5921=CARTESIAN_POINT('Ctrl Pts',(1.2600586328202,0.32583616303801,-0.153092633895047));
#5922=CARTESIAN_POINT('Ctrl Pts',(1.27550420984285,0.35,-0.132658480043447));
#5923=CARTESIAN_POINT('Origin',(1.1,0.35,0.));
#5924=CARTESIAN_POINT('Origin',(-0.339918693812442,0.,1.04616216792467));
#5925=CARTESIAN_POINT('',(-0.559918693812442,0.,1.04616216792467));
#5926=CARTESIAN_POINT('Origin',(-0.339918693812442,0.,1.04616216792467));
#5927=CARTESIAN_POINT('',(-0.559918693812442,0.260874438760115,1.04616216792418));
#5928=CARTESIAN_POINT('',(-0.559918693812442,0.,1.04616216792467));
#5929=CARTESIAN_POINT('',(-0.52031818912536,0.35,1.17208286555157));
#5930=CARTESIAN_POINT('Ctrl Pts',(-0.52031818912536,0.35,1.17208286555157));
#5931=CARTESIAN_POINT('Ctrl Pts',(-0.529217457694123,0.335332571878444,
1.15933338442007));
#5932=CARTESIAN_POINT('Ctrl Pts',(-0.537396458457103,0.321517770338583,
1.14467059284705));
#5933=CARTESIAN_POINT('Ctrl Pts',(-0.550248212225112,0.296532793702566,
1.11286085586034));
#5934=CARTESIAN_POINT('Ctrl Pts',(-0.555078018641098,0.285216775966753,
1.09565550010774));
#5935=CARTESIAN_POINT('Ctrl Pts',(-0.559145317472554,0.270067412950761,
1.06722515592215));
#5936=CARTESIAN_POINT('Ctrl Pts',(-0.559918693812443,0.265170116534296,
1.05680550414918));
#5937=CARTESIAN_POINT('Ctrl Pts',(-0.559918693812443,0.260874438760115,
1.0461621679237));
#5938=CARTESIAN_POINT('',(-0.267986765351098,0.35,1.25407031511432));
#5939=CARTESIAN_POINT('Origin',(-0.339918693812442,0.35,1.04616216792467));
#5940=CARTESIAN_POINT('',(-0.174765758038764,0.35,0.900819442598166));
#5941=CARTESIAN_POINT('Ctrl Pts',(-0.174765758038764,0.35,0.900819442598166));
#5942=CARTESIAN_POINT('Ctrl Pts',(-0.16615910126156,0.335479408675346,0.910599186515575));
#5943=CARTESIAN_POINT('Ctrl Pts',(-0.157611943697822,0.321649098925924,
0.922105787154341));
#5944=CARTESIAN_POINT('Ctrl Pts',(-0.142410854924046,0.296417377297428,
0.948090475176036));
#5945=CARTESIAN_POINT('Ctrl Pts',(-0.135635598256597,0.284856881183445,
0.962749516762522));
#5946=CARTESIAN_POINT('Ctrl Pts',(-0.124807600924643,0.26429242669275,0.996493855518018));
#5947=CARTESIAN_POINT('Ctrl Pts',(-0.12107905659851,0.255687624123886,1.01568738120414));
#5948=CARTESIAN_POINT('Ctrl Pts',(-0.11927397960075,0.244553314150373,1.05530113820794));
#5949=CARTESIAN_POINT('Ctrl Pts',(-0.120893383895271,0.241869161316321,
1.07486553219761));
#5950=CARTESIAN_POINT('Ctrl Pts',(-0.129925208402574,0.242150819014083,
1.11515786183808));
#5951=CARTESIAN_POINT('Ctrl Pts',(-0.137545730009388,0.245541115579871,
1.13486353269143));
#5952=CARTESIAN_POINT('Ctrl Pts',(-0.159894075495139,0.25896926022056,1.17516872094799));
#5953=CARTESIAN_POINT('Ctrl Pts',(-0.175488151194729,0.270150443771654,
1.19412647612185));
#5954=CARTESIAN_POINT('Ctrl Pts',(-0.216960528286492,0.30273418323525,1.2315190249125));
#5955=CARTESIAN_POINT('Ctrl Pts',(-0.243776713476772,0.325833097600423,
1.24569413677302));
#5956=CARTESIAN_POINT('Ctrl Pts',(-0.267986765351098,0.35,1.25407031511432));
#5957=CARTESIAN_POINT('',(-0.388099915049348,0.35,0.831502973106184));
#5958=CARTESIAN_POINT('Origin',(-0.339918693812442,0.35,1.04616216792467));
#5959=CARTESIAN_POINT('Ctrl Pts',(-0.559918693812442,0.260874438760115,
1.0461621679237));
#5960=CARTESIAN_POINT('Ctrl Pts',(-0.559918693812441,0.256572067929757,
1.03550224841356));
#5961=CARTESIAN_POINT('Ctrl Pts',(-0.55914412823418,0.252872176837747,1.02461835660205));
#5962=CARTESIAN_POINT('Ctrl Pts',(-0.554627960771623,0.244745328150166,
0.994433608378459));
#5963=CARTESIAN_POINT('Ctrl Pts',(-0.549175023311743,0.241941375180247,
0.975354466173215));
#5964=CARTESIAN_POINT('Ctrl Pts',(-0.532711855060331,0.242062069598183,
0.938206075044726));
#5965=CARTESIAN_POINT('Ctrl Pts',(-0.521946739366383,0.245143826724662,
0.921041750757786));
#5966=CARTESIAN_POINT('Ctrl Pts',(-0.494476822014916,0.25808943656053,0.887869891643464));
#5967=CARTESIAN_POINT('Ctrl Pts',(-0.477731860324512,0.268767859044401,
0.873445791067852));
#5968=CARTESIAN_POINT('Ctrl Pts',(-0.435054453498551,0.301421636034264,
0.84547220309525));
#5969=CARTESIAN_POINT('Ctrl Pts',(-0.409474560891576,0.325582986157859,
0.836300608451158));
#5970=CARTESIAN_POINT('Ctrl Pts',(-0.388099915049348,0.35,0.831502973106184));
#5971=CARTESIAN_POINT('Origin',(0.889918693812442,0.,0.64656377752172));
#5972=CARTESIAN_POINT('',(0.669918693812442,0.,0.64656377752172));
#5973=CARTESIAN_POINT('Origin',(0.889918693812442,0.,0.64656377752172));
#5974=CARTESIAN_POINT('',(0.669918693812442,0.328688122539757,0.646563777561565));
#5975=CARTESIAN_POINT('',(0.669918693812442,0.,0.64656377752172));
#5976=CARTESIAN_POINT('',(0.953929883998579,0.35,0.857045528585688));
#5977=CARTESIAN_POINT('Ctrl Pts',(0.953929883998579,0.35,0.857045528585689));
#5978=CARTESIAN_POINT('Ctrl Pts',(0.939113614143973,0.335390975831827,0.861551415973636));
#5979=CARTESIAN_POINT('Ctrl Pts',(0.922713318211476,0.32162844535795,0.864791301338213));
#5980=CARTESIAN_POINT('Ctrl Pts',(0.888689691679126,0.296761201350329,0.867202773669637));
#5981=CARTESIAN_POINT('Ctrl Pts',(0.87096870334968,0.285505993520706,0.866515344265356));
#5982=CARTESIAN_POINT('Ctrl Pts',(0.832657955828335,0.264913063744833,0.859966994580058));
#5983=CARTESIAN_POINT('Ctrl Pts',(0.812042610895507,0.255983013500831,0.853529132681505));
#5984=CARTESIAN_POINT('Ctrl Pts',(0.774637004578398,0.244799211872409,0.834944631013122));
#5985=CARTESIAN_POINT('Ctrl Pts',(0.758129671802899,0.241962745238242,0.823863745365518));
#5986=CARTESIAN_POINT('Ctrl Pts',(0.72783201892456,0.242038904448235,0.796734896229851));
#5987=CARTESIAN_POINT('Ctrl Pts',(0.714819045120535,0.245095813663096,0.781209421868765));
#5988=CARTESIAN_POINT('Ctrl Pts',(0.691707150272297,0.257996207173293,0.744838566725142));
#5989=CARTESIAN_POINT('Ctrl Pts',(0.683135660593065,0.268662345405231,0.724442597621042));
#5990=CARTESIAN_POINT('Ctrl Pts',(0.672013600394921,0.29561651331323,0.683754327616304));
#5991=CARTESIAN_POINT('Ctrl Pts',(0.669918693818778,0.311769951237127,0.664055407862726));
#5992=CARTESIAN_POINT('Ctrl Pts',(0.669918693812442,0.328688122539757,0.646563777601409));
#5993=CARTESIAN_POINT('',(1.10987928032073,0.35,0.642399598979491));
#5994=CARTESIAN_POINT('Origin',(0.889918693812442,0.35,0.64656377752172));
#5995=CARTESIAN_POINT('',(0.802724611619556,0.35,0.444580629634229));
#5996=CARTESIAN_POINT('Ctrl Pts',(0.802724611619556,0.35,0.444580629634229));
#5997=CARTESIAN_POINT('Ctrl Pts',(0.814693298418458,0.335469703254327,0.439413868588077));
#5998=CARTESIAN_POINT('Ctrl Pts',(0.828288194978147,0.321630486900879,0.434838103866291));
#5999=CARTESIAN_POINT('Ctrl Pts',(0.857626293279467,0.296466623645907,0.428430764212231));
#6000=CARTESIAN_POINT('Ctrl Pts',(0.873562500583475,0.284968850954313,0.426522755127025));
#6001=CARTESIAN_POINT('Ctrl Pts',(0.908944175205009,0.264389371081103,0.426610046318699));
#6002=CARTESIAN_POINT('Ctrl Pts',(0.928411894256451,0.255739222721824,0.428985062409479));
#6003=CARTESIAN_POINT('Ctrl Pts',(0.966701070362238,0.244572490203357,0.439509162402782));
#6004=CARTESIAN_POINT('Ctrl Pts',(0.984800606765884,0.24187970665778,0.447081989738821));
#6005=CARTESIAN_POINT('Ctrl Pts',(1.02033222655978,0.242137933247099,0.468098181585364));
#6006=CARTESIAN_POINT('Ctrl Pts',(1.03672671564999,0.245516880218307,0.48142671327546));
#6007=CARTESIAN_POINT('Ctrl Pts',(1.0681914718434,0.258930838869849,0.515141616697554));
#6008=CARTESIAN_POINT('Ctrl Pts',(1.08142350523446,0.270117119131827,0.535848665318464));
#6009=CARTESIAN_POINT('Ctrl Pts',(1.10419503710793,0.302714929726697,0.586877157140452));
#6010=CARTESIAN_POINT('Ctrl Pts',(1.10939416747485,0.325822565838313,0.616774927746317));
#6011=CARTESIAN_POINT('Ctrl Pts',(1.10987928032073,0.35,0.642399598979492));
#6012=CARTESIAN_POINT('',(0.670876851625708,0.35,0.626053502744384));
#6013=CARTESIAN_POINT('Origin',(0.889918693812442,0.35,0.64656377752172));
#6014=CARTESIAN_POINT('Ctrl Pts',(0.669918693812442,0.328688122539757,0.646563777601409));
#6015=CARTESIAN_POINT('Ctrl Pts',(0.669918693809818,0.335695203413973,0.639319184455347));
#6016=CARTESIAN_POINT('Ctrl Pts',(0.670277510265801,0.342834510102275,0.632454237839257));
#6017=CARTESIAN_POINT('Ctrl Pts',(0.670876851625708,0.35,0.626053502744384));
#6018=CARTESIAN_POINT('Origin',(0.339918693812442,0.,1.04616216792467));
#6019=CARTESIAN_POINT('',(0.119918693812442,0.,1.04616216792467));
#6020=CARTESIAN_POINT('Origin',(0.339918693812442,0.,1.04616216792467));
#6021=CARTESIAN_POINT('',(0.119918693812442,0.247376716776579,1.04616216792467));
#6022=CARTESIAN_POINT('',(0.119918693812442,0.,1.04616216792467));
#6023=CARTESIAN_POINT('',(0.267986765351098,0.35,1.25407031511432));
#6024=CARTESIAN_POINT('Ctrl Pts',(0.267986765351098,0.35,1.25407031511432));
#6025=CARTESIAN_POINT('Ctrl Pts',(0.253293148857988,0.335332571878444,1.24898662703038));
#6026=CARTESIAN_POINT('Ctrl Pts',(0.238057625599671,0.321517770338583,1.2419316754898));
#6027=CARTESIAN_POINT('Ctrl Pts',(0.20896304411374,0.296532793702567,1.22375112901188));
#6028=CARTESIAN_POINT('Ctrl Pts',(0.194942594271844,0.285216775966753,1.21267059279651));
#6029=CARTESIAN_POINT('Ctrl Pts',(0.16782911650589,0.264680669899338,1.18473227113195));
#6030=CARTESIAN_POINT('Ctrl Pts',(0.155029153917439,0.255831783241443,1.16745023332297));
#6031=CARTESIAN_POINT('Ctrl Pts',(0.135809963569083,0.244745328150166,1.13051582480638));
#6032=CARTESIAN_POINT('Ctrl Pts',(0.129007044228756,0.241941375180247,1.11187531830365));
#6033=CARTESIAN_POINT('Ctrl Pts',(0.121501840920506,0.242047740248445,1.07686180187776));
#6034=CARTESIAN_POINT('Ctrl Pts',(0.119918693812442,0.243865919483247,1.06140091782046));
#6035=CARTESIAN_POINT('Ctrl Pts',(0.119918693812442,0.247376716776579,1.04616216792467));
#6036=CARTESIAN_POINT('',(0.52031818912536,0.35,1.17208286555157));
#6037=CARTESIAN_POINT('Origin',(0.339918693812442,0.35,1.04616216792467));
#6038=CARTESIAN_POINT('',(0.388099915049348,0.35,0.831502973106184));
#6039=CARTESIAN_POINT('Ctrl Pts',(0.388099915049349,0.35,0.831502973106184));
#6040=CARTESIAN_POINT('Ctrl Pts',(0.400811235892708,0.335479408675346,0.83435608621082));
#6041=CARTESIAN_POINT('Ctrl Pts',(0.414489441774859,0.321649098925924,0.838641228510082));
#6042=CARTESIAN_POINT('Ctrl Pts',(0.442060797330419,0.296417377297427,0.85072830691315));
#6043=CARTESIAN_POINT('Ctrl Pts',(0.456158463572915,0.284856881183445,0.858605324728243));
#6044=CARTESIAN_POINT('Ctrl Pts',(0.484752922098352,0.264292426692752,0.879540531101798));
#6045=CARTESIAN_POINT('Ctrl Pts',(0.499051049160275,0.255687624123886,0.892876836196423));
#6046=CARTESIAN_POINT('Ctrl Pts',(0.523795769282349,0.244553314150373,0.923864041185));
#6047=CARTESIAN_POINT('Ctrl Pts',(0.533985305944486,0.241869161316321,0.940643830369109));
#6048=CARTESIAN_POINT('Ctrl Pts',(0.550361643571045,0.242150819014083,0.9785497830379));
#6049=CARTESIAN_POINT('Ctrl Pts',(0.555779214799254,0.245541115579872,0.998971235859074));
#6050=CARTESIAN_POINT('Ctrl Pts',(0.561389818753198,0.25896926022056,1.04471484600977));
#6051=CARTESIAN_POINT('Ctrl Pts',(0.559917035408429,0.270150443771653,1.06921795983998));
#6052=CARTESIAN_POINT('Ctrl Pts',(0.548343966268834,0.30273418323525,1.12384601890666));
#6053=CARTESIAN_POINT('Ctrl Pts',(0.534981138426803,0.325833097600422,1.15107608347657));
#6054=CARTESIAN_POINT('Ctrl Pts',(0.52031818912536,0.35,1.17208286555157));
#6055=CARTESIAN_POINT('',(0.174765758038764,0.35,0.900819442598166));
#6056=CARTESIAN_POINT('Origin',(0.339918693812442,0.35,1.04616216792467));
#6057=CARTESIAN_POINT('Ctrl Pts',(0.119918693812442,0.247376716776579,1.04616216792467));
#6058=CARTESIAN_POINT('Ctrl Pts',(0.119918693812442,0.248451342886481,1.04149771220363));
#6059=CARTESIAN_POINT('Ctrl Pts',(0.120067055145306,0.249684690290744,1.03685410010078));
#6060=CARTESIAN_POINT('Ctrl Pts',(0.121836675927961,0.25808943656053,1.00894801471422));
#6061=CARTESIAN_POINT('Ctrl Pts',(0.126905360909727,0.268767859044402,0.987436230688157));
#6062=CARTESIAN_POINT('Ctrl Pts',(0.144989645843781,0.301421636034262,0.939719972286297));
#6063=CARTESIAN_POINT('Ctrl Pts',(0.160293285605306,0.325582986157856,0.917264512724103));
#6064=CARTESIAN_POINT('Ctrl Pts',(0.174765758038763,0.35,0.900819442598166));
#6065=CARTESIAN_POINT('Origin',(-0.889918693812442,0.,0.646563777521721));
#6066=CARTESIAN_POINT('',(-1.10991869381244,0.,0.646563777521721));
#6067=CARTESIAN_POINT('Origin',(-0.889918693812442,0.,0.646563777521721));
#6068=CARTESIAN_POINT('',(-1.10991869381244,0.35,0.646563777521721));
#6069=CARTESIAN_POINT('',(-1.10991869381244,0.,0.646563777521721));
#6070=CARTESIAN_POINT('',(-0.953929883998579,0.35,0.857045528585689));
#6071=CARTESIAN_POINT('Origin',(-0.889918693812442,0.35,0.646563777521721));
#6072=CARTESIAN_POINT('',(-0.670876851625708,0.35,0.626053502744384));
#6073=CARTESIAN_POINT('Ctrl Pts',(-0.670876851625708,0.35,0.626053502744384));
#6074=CARTESIAN_POINT('Ctrl Pts',(-0.669661497485836,0.335469703254326,
0.639033017285111));
#6075=CARTESIAN_POINT('Ctrl Pts',(-0.669510740703862,0.321630486900879,
0.653376521307855));
#6076=CARTESIAN_POINT('Ctrl Pts',(-0.672482969531502,0.296466623645907,
0.68325868771487));
#6077=CARTESIAN_POINT('Ctrl Pts',(-0.675592903940688,0.284968850954313,
0.699004528749127));
#6078=CARTESIAN_POINT('Ctrl Pts',(-0.686609461544843,0.264389371081103,
0.732627526493686));
#6079=CARTESIAN_POINT('Ctrl Pts',(-0.694884092102898,0.255739222721824,
0.750408507220998));
#6080=CARTESIAN_POINT('Ctrl Pts',(-0.716725112096974,0.244572490203356,
0.783571551911549));
#6081=CARTESIAN_POINT('Ctrl Pts',(-0.729520363220728,0.24187970665778,0.798445101607853));
#6082=CARTESIAN_POINT('Ctrl Pts',(-0.760487823778074,0.242137933247099,
0.825743319709735));
#6083=CARTESIAN_POINT('Ctrl Pts',(-0.778230186437554,0.245516880218307,
0.837216662588005));
#6084=CARTESIAN_POINT('Ctrl Pts',(-0.820018109421027,0.258930838869848,
0.856722945878246));
#6085=CARTESIAN_POINT('Ctrl Pts',(-0.843800606133157,0.270117119131826,
0.862908527531438));
#6086=CARTESIAN_POINT('Ctrl Pts',(-0.899368376134038,0.302714929726702,
0.868796870135415));
#6087=CARTESIAN_POINT('Ctrl Pts',(-0.929409465330792,0.325822565838321,
0.864502617738802));
#6088=CARTESIAN_POINT('Ctrl Pts',(-0.95392988399858,0.35,0.857045528585688));
#6089=CARTESIAN_POINT('',(-0.802724611619556,0.35,0.444580629634229));
#6090=CARTESIAN_POINT('Origin',(-0.889918693812442,0.35,0.646563777521721));
#6091=CARTESIAN_POINT('',(-1.10987928032073,0.35,0.642399598979491));
#6092=CARTESIAN_POINT('Ctrl Pts',(-1.10987928032073,0.35,0.642399598979492));
#6093=CARTESIAN_POINT('Ctrl Pts',(-1.10958615470441,0.335390975831827,0.626916093209464));
#6094=CARTESIAN_POINT('Ctrl Pts',(-1.10759949863652,0.321628445357949,0.610317305256213));
#6095=CARTESIAN_POINT('Ctrl Pts',(-1.09937906630242,0.296761201350329,0.577213727602755));
#6096=CARTESIAN_POINT('Ctrl Pts',(-1.09324919553707,0.285505993520706,0.5605724935452));
#6097=CARTESIAN_POINT('Ctrl Pts',(-1.07518267284658,0.264913063744833,0.526160358808755));
#6098=CARTESIAN_POINT('Ctrl Pts',(-1.06268941040781,0.255983013500831,0.508543409408808));
#6099=CARTESIAN_POINT('Ctrl Pts',(-1.03345553095711,0.244799211872409,0.478711490622469));
#6100=CARTESIAN_POINT('Ctrl Pts',(-1.0178159360962,0.241962745238242,0.466436266197514));
#6101=CARTESIAN_POINT('Ctrl Pts',(-0.982652377717061,0.242038904448235,
0.446004761419877));
#6102=CARTESIAN_POINT('Ctrl Pts',(-0.963865544104578,0.245095813663095,
0.438426323310488));
#6103=CARTESIAN_POINT('Ctrl Pts',(-0.922132837036694,0.257996207173294,
0.427684817450471));
#6104=CARTESIAN_POINT('Ctrl Pts',(-0.900086381736091,0.268662345405233,
0.425835547406596));
#6105=CARTESIAN_POINT('Ctrl Pts',(-0.849024073352861,0.301328368152829,
0.428254106385369));
#6106=CARTESIAN_POINT('Ctrl Pts',(-0.822877500049854,0.325533869830937,
0.435880831514466));
#6107=CARTESIAN_POINT('Ctrl Pts',(-0.802724611619556,0.35,0.444580629634229));
#6108=CARTESIAN_POINT('Origin',(-0.889918693812442,0.35,0.646563777521721));
#6109=CARTESIAN_POINT('Origin',(-1.1,0.,1.34711147906209E-16));
#6110=CARTESIAN_POINT('',(-1.32,0.,1.61653377487451E-16));
#6111=CARTESIAN_POINT('Origin',(-1.1,0.,1.34711147906209E-16));
#6112=CARTESIAN_POINT('',(-1.32,0.35,1.61653377487451E-16));
#6113=CARTESIAN_POINT('',(-1.32,0.,1.61653377487451E-16));
#6114=CARTESIAN_POINT('',(-1.27550420984285,0.35,0.132658480043447));
#6115=CARTESIAN_POINT('Origin',(-1.1,0.35,1.34711147906209E-16));
#6116=CARTESIAN_POINT('',(-0.910735790157152,0.35,0.112156403618172));
#6117=CARTESIAN_POINT('Ctrl Pts',(-0.910735790157152,0.35,0.112156403618173));
#6118=CARTESIAN_POINT('Ctrl Pts',(-0.917376089752458,0.335482002504965,
0.123361925688084));
#6119=CARTESIAN_POINT('Ctrl Pts',(-0.925676503375737,0.321654073155954,
0.135044303040797));
#6120=CARTESIAN_POINT('Ctrl Pts',(-0.945705763566752,0.296402587659025,
0.157548233557298));
#6121=CARTESIAN_POINT('Ctrl Pts',(-0.957575956315956,0.284823988089694,
0.168539952403237));
#6122=CARTESIAN_POINT('Ctrl Pts',(-0.986343324120607,0.264264067609,0.189265250815529));
#6123=CARTESIAN_POINT('Ctrl Pts',(-1.00343254919411,0.255672471019212,0.198729556237649));
#6124=CARTESIAN_POINT('Ctrl Pts',(-1.04053658704398,0.24454764112274,0.21267781162389));
#6125=CARTESIAN_POINT('Ctrl Pts',(-1.05964780090184,0.241866044436253,0.217181471497844));
#6126=CARTESIAN_POINT('Ctrl Pts',(-1.1007627783985,0.242154653351498,0.221036398352684));
#6127=CARTESIAN_POINT('Ctrl Pts',(-1.12185832284616,0.24554830260434,0.219874810080966));
#6128=CARTESIAN_POINT('Ctrl Pts',(-1.16708666484378,0.258980602991006,0.211069922924208));
#6129=CARTESIAN_POINT('Ctrl Pts',(-1.18992721371268,0.270160239182283,0.202098025620397));
#6130=CARTESIAN_POINT('Ctrl Pts',(-1.23829403807689,0.302739787597863,0.174213524003119));
#6131=CARTESIAN_POINT('Ctrl Pts',(-1.2600586328202,0.325836163038011,0.153092633895046));
#6132=CARTESIAN_POINT('Ctrl Pts',(-1.27550420984285,0.35,0.132658480043447));
#6133=CARTESIAN_POINT('',(-0.910735790157152,0.35,-0.112156403618172));
#6134=CARTESIAN_POINT('Origin',(-1.1,0.35,1.34711147906209E-16));
#6135=CARTESIAN_POINT('',(-1.27550420984285,0.35,-0.132658480043447));
#6136=CARTESIAN_POINT('Ctrl Pts',(-1.27550420984285,0.35,-0.132658480043447));
#6137=CARTESIAN_POINT('Ctrl Pts',(-1.26611782177473,0.335315462762739,-0.145076462072449));
#6138=CARTESIAN_POINT('Ctrl Pts',(-1.25468431627751,0.321485352158938,-0.157400492027332));
#6139=CARTESIAN_POINT('Ctrl Pts',(-1.22835219222699,0.296466041103173,-0.179483010322184));
#6140=CARTESIAN_POINT('Ctrl Pts',(-1.21344338101808,0.285132356747975,-0.189407731207313));
#6141=CARTESIAN_POINT('Ctrl Pts',(-1.17846267135551,0.264612821304931,-0.206540975098488));
#6142=CARTESIAN_POINT('Ctrl Pts',(-1.15809147022147,0.255787504332734,-0.213351934557227));
#6143=CARTESIAN_POINT('Ctrl Pts',(-1.11706033563968,0.24472949208419,-0.220191916744402));
#6144=CARTESIAN_POINT('Ctrl Pts',(-1.09724086630217,0.241935102766417,-0.22089327619843));
#6145=CARTESIAN_POINT('Ctrl Pts',(-1.05683477389847,0.242068991386358,-0.216703862540943));
#6146=CARTESIAN_POINT('Ctrl Pts',(-1.03718465931368,0.245158125533072,-0.211762979306542));
#6147=CARTESIAN_POINT('Ctrl Pts',(-0.997159417898573,0.258117110209497,
-0.195877882014933));
#6148=CARTESIAN_POINT('Ctrl Pts',(-0.978275892037171,0.268799087403243,
-0.184408191234793));
#6149=CARTESIAN_POINT('Ctrl Pts',(-0.938511832204561,0.301449132027478,
-0.152471662943099));
#6150=CARTESIAN_POINT('Ctrl Pts',(-0.92189712024416,0.325597462144781,-0.130991175878742));
#6151=CARTESIAN_POINT('Ctrl Pts',(-0.910735790157152,0.35,-0.112156403618172));
#6152=CARTESIAN_POINT('Origin',(-1.1,0.35,1.34711147906209E-16));
#6153=CARTESIAN_POINT('Origin',(-0.339918693812442,0.,-1.04616216792467));
#6154=CARTESIAN_POINT('',(-0.559918693812442,0.,-1.04616216792467));
#6155=CARTESIAN_POINT('Origin',(-0.339918693812442,0.,-1.04616216792467));
#6156=CARTESIAN_POINT('',(-0.559918693812442,0.26087443875944,-1.04616216792335));
#6157=CARTESIAN_POINT('',(-0.559918693812442,0.,-1.04616216792467));
#6158=CARTESIAN_POINT('',(-0.388099915049348,0.35,-0.831502973106184));
#6159=CARTESIAN_POINT('Ctrl Pts',(-0.388099915049349,0.35,-0.831502973106184));
#6160=CARTESIAN_POINT('Ctrl Pts',(-0.400811235892708,0.335479408675346,
-0.83435608621082));
#6161=CARTESIAN_POINT('Ctrl Pts',(-0.414489441774859,0.321649098925924,
-0.838641228510082));
#6162=CARTESIAN_POINT('Ctrl Pts',(-0.442060797330419,0.296417377297428,
-0.85072830691315));
#6163=CARTESIAN_POINT('Ctrl Pts',(-0.456158463572915,0.284856881183445,
-0.858605324728243));
#6164=CARTESIAN_POINT('Ctrl Pts',(-0.484752922098354,0.264292426692751,
-0.879540531101799));
#6165=CARTESIAN_POINT('Ctrl Pts',(-0.499051049160275,0.255687624123886,
-0.892876836196423));
#6166=CARTESIAN_POINT('Ctrl Pts',(-0.523795769282349,0.244553314150373,
-0.923864041185001));
#6167=CARTESIAN_POINT('Ctrl Pts',(-0.533985305944486,0.241869161316321,
-0.94064383036911));
#6168=CARTESIAN_POINT('Ctrl Pts',(-0.550361643571044,0.242150819014083,
-0.9785497830379));
#6169=CARTESIAN_POINT('Ctrl Pts',(-0.555779214799254,0.245541115579872,
-0.998971235859074));
#6170=CARTESIAN_POINT('Ctrl Pts',(-0.559392545156815,0.254189083441125,
-1.02843094760825));
#6171=CARTESIAN_POINT('Ctrl Pts',(-0.559918693812337,0.257327896059345,
-1.03737495240447));
#6172=CARTESIAN_POINT('Ctrl Pts',(-0.559918693812442,0.26087443875944,-1.04616216792202));
#6173=CARTESIAN_POINT('',(-0.174765758038764,0.35,-0.900819442598166));
#6174=CARTESIAN_POINT('Origin',(-0.339918693812442,0.35,-1.04616216792467));
#6175=CARTESIAN_POINT('',(-0.267986765351098,0.35,-1.25407031511432));
#6176=CARTESIAN_POINT('Ctrl Pts',(-0.267986765351098,0.35,-1.25407031511432));
#6177=CARTESIAN_POINT('Ctrl Pts',(-0.253293148857987,0.335332571878443,
-1.24898662703038));
#6178=CARTESIAN_POINT('Ctrl Pts',(-0.23805762559967,0.321517770338583,-1.2419316754898));
#6179=CARTESIAN_POINT('Ctrl Pts',(-0.208963044113739,0.296532793702567,
-1.22375112901188));
#6180=CARTESIAN_POINT('Ctrl Pts',(-0.194942594271844,0.285216775966753,
-1.21267059279651));
#6181=CARTESIAN_POINT('Ctrl Pts',(-0.167829116505892,0.264680669899339,
-1.18473227113195));
#6182=CARTESIAN_POINT('Ctrl Pts',(-0.155029153917439,0.255831783241444,
-1.16745023332297));
#6183=CARTESIAN_POINT('Ctrl Pts',(-0.135809963569083,0.244745328150166,
-1.13051582480638));
#6184=CARTESIAN_POINT('Ctrl Pts',(-0.129007044228756,0.241941375180247,
-1.11187531830365));
#6185=CARTESIAN_POINT('Ctrl Pts',(-0.120490750673684,0.242062069598183,
-1.07214483106283));
#6186=CARTESIAN_POINT('Ctrl Pts',(-0.119110975535071,0.245143826724661,
-1.05193102477361));
#6187=CARTESIAN_POINT('Ctrl Pts',(-0.121836675927961,0.25808943656053,-1.00894801471422));
#6188=CARTESIAN_POINT('Ctrl Pts',(-0.126905360909727,0.268767859044401,
-0.987436230688157));
#6189=CARTESIAN_POINT('Ctrl Pts',(-0.144989645843782,0.301421636034265,
-0.939719972286292));
#6190=CARTESIAN_POINT('Ctrl Pts',(-0.160293285605309,0.325582986157861,
-0.9172645127241));
#6191=CARTESIAN_POINT('Ctrl Pts',(-0.174765758038764,0.35,-0.900819442598166));
#6192=CARTESIAN_POINT('',(-0.52031818912536,0.35,-1.17208286555157));
#6193=CARTESIAN_POINT('Origin',(-0.339918693812442,0.35,-1.04616216792467));
#6194=CARTESIAN_POINT('Ctrl Pts',(-0.559918693812442,0.26087443875944,-1.04616216792202));
#6195=CARTESIAN_POINT('Ctrl Pts',(-0.559918693812632,0.267254559470881,
-1.0619700970689));
#6196=CARTESIAN_POINT('Ctrl Pts',(-0.558211019996387,0.274953695271867,
-1.07727082028465));
#6197=CARTESIAN_POINT('Ctrl Pts',(-0.548343966268835,0.302734183235248,
-1.12384601890665));
#6198=CARTESIAN_POINT('Ctrl Pts',(-0.534981138426805,0.325833097600418,
-1.15107608347657));
#6199=CARTESIAN_POINT('Ctrl Pts',(-0.52031818912536,0.35,-1.17208286555157));
#6200=CARTESIAN_POINT('Origin',(0.889918693812442,0.,-0.646563777521721));
#6201=CARTESIAN_POINT('',(0.669918693812442,0.,-0.646563777521721));
#6202=CARTESIAN_POINT('Origin',(0.889918693812442,0.,-0.646563777521721));
#6203=CARTESIAN_POINT('',(0.669918693812442,0.328688122609646,-0.646563777525436));
#6204=CARTESIAN_POINT('',(0.669918693812442,0.,-0.646563777521721));
#6205=CARTESIAN_POINT('',(0.670876851625708,0.35,-0.626053502744384));
#6206=CARTESIAN_POINT('Ctrl Pts',(0.670876851625708,0.35,-0.626053502744384));
#6207=CARTESIAN_POINT('Ctrl Pts',(0.670266054477489,0.34269754919667,-0.632576581250196));
#6208=CARTESIAN_POINT('Ctrl Pts',(0.669918693812202,0.335572060345374,-0.639446501589323));
#6209=CARTESIAN_POINT('Ctrl Pts',(0.669918693812442,0.328688122609646,-0.646563777529151));
#6210=CARTESIAN_POINT('',(0.802724611619556,0.35,-0.444580629634229));
#6211=CARTESIAN_POINT('Origin',(0.889918693812442,0.35,-0.646563777521721));
#6212=CARTESIAN_POINT('',(1.10987928032073,0.35,-0.642399598979491));
#6213=CARTESIAN_POINT('Ctrl Pts',(1.10987928032073,0.35,-0.642399598979492));
#6214=CARTESIAN_POINT('Ctrl Pts',(1.10958615470441,0.335390975831828,-0.626916093209466));
#6215=CARTESIAN_POINT('Ctrl Pts',(1.10759949863652,0.32162844535795,-0.610317305256214));
#6216=CARTESIAN_POINT('Ctrl Pts',(1.09937906630242,0.296761201350329,-0.577213727602755));
#6217=CARTESIAN_POINT('Ctrl Pts',(1.09324919553707,0.285505993520706,-0.560572493545201));
#6218=CARTESIAN_POINT('Ctrl Pts',(1.07518267284658,0.264913063744833,-0.526160358808756));
#6219=CARTESIAN_POINT('Ctrl Pts',(1.06268941040781,0.255983013500831,-0.508543409408808));
#6220=CARTESIAN_POINT('Ctrl Pts',(1.03345553095711,0.244799211872409,-0.478711490622469));
#6221=CARTESIAN_POINT('Ctrl Pts',(1.0178159360962,0.241962745238242,-0.466436266197514));
#6222=CARTESIAN_POINT('Ctrl Pts',(0.982652377717061,0.242038904448235,-0.446004761419877));
#6223=CARTESIAN_POINT('Ctrl Pts',(0.963865544104578,0.245095813663095,-0.438426323310488));
#6224=CARTESIAN_POINT('Ctrl Pts',(0.922132837036694,0.257996207173294,-0.427684817450471));
#6225=CARTESIAN_POINT('Ctrl Pts',(0.900086381736092,0.268662345405233,-0.425835547406596));
#6226=CARTESIAN_POINT('Ctrl Pts',(0.849024073352859,0.30132836815283,-0.428254106385369));
#6227=CARTESIAN_POINT('Ctrl Pts',(0.822877500049852,0.32553386983094,-0.435880831514467));
#6228=CARTESIAN_POINT('Ctrl Pts',(0.802724611619556,0.35,-0.444580629634229));
#6229=CARTESIAN_POINT('',(0.953929883998579,0.35,-0.857045528585689));
#6230=CARTESIAN_POINT('Origin',(0.889918693812442,0.35,-0.646563777521721));
#6231=CARTESIAN_POINT('Ctrl Pts',(0.669918693812442,0.328688122609646,-0.646563777529151));
#6232=CARTESIAN_POINT('Ctrl Pts',(0.66991869381268,0.32187451403212,-0.65360834043107));
#6233=CARTESIAN_POINT('Ctrl Pts',(0.670258663808197,0.31529832480498,-0.66089598362366));
#6234=CARTESIAN_POINT('Ctrl Pts',(0.672482969531502,0.296466623645907,-0.68325868771487));
#6235=CARTESIAN_POINT('Ctrl Pts',(0.675592903940687,0.284968850954313,-0.699004528749128));
#6236=CARTESIAN_POINT('Ctrl Pts',(0.686609461544843,0.264389371081104,-0.732627526493686));
#6237=CARTESIAN_POINT('Ctrl Pts',(0.694884092102897,0.255739222721825,-0.750408507220998));
#6238=CARTESIAN_POINT('Ctrl Pts',(0.716725112096974,0.244572490203356,-0.783571551911549));
#6239=CARTESIAN_POINT('Ctrl Pts',(0.729520363220727,0.24187970665778,-0.798445101607854));
#6240=CARTESIAN_POINT('Ctrl Pts',(0.760487823778074,0.242137933247099,-0.825743319709736));
#6241=CARTESIAN_POINT('Ctrl Pts',(0.778230186437555,0.245516880218307,-0.837216662588005));
#6242=CARTESIAN_POINT('Ctrl Pts',(0.820018109421027,0.258930838869848,-0.856722945878246));
#6243=CARTESIAN_POINT('Ctrl Pts',(0.843800606133157,0.270117119131827,-0.862908527531438));
#6244=CARTESIAN_POINT('Ctrl Pts',(0.899368376134036,0.302714929726701,-0.868796870135415));
#6245=CARTESIAN_POINT('Ctrl Pts',(0.92940946533079,0.325822565838319,-0.864502617738803));
#6246=CARTESIAN_POINT('Ctrl Pts',(0.953929883998579,0.35,-0.857045528585689));
#6247=CARTESIAN_POINT('Origin',(1.4,0.35,0.));
#6248=CARTESIAN_POINT('Origin',(0.,0.35,0.));
#6249=CARTESIAN_POINT('Origin',(0.,0.35,0.));
#6250=CARTESIAN_POINT('Origin',(0.,0.35,0.));
#6251=CARTESIAN_POINT('Origin',(0.,0.35,0.));
#6252=CARTESIAN_POINT('Origin',(0.,0.35,0.));
#6253=CARTESIAN_POINT('Origin',(0.,0.35,0.));
#6254=CARTESIAN_POINT('Origin',(0.,0.35,0.));
#6255=CARTESIAN_POINT('Origin',(0.,0.35,0.));
#6256=CARTESIAN_POINT('Origin',(0.,0.35,0.));
#6257=CARTESIAN_POINT('Origin',(0.,0.35,0.));
#6258=CARTESIAN_POINT('',(-0.75,0.35,-9.18485099360515E-17));
#6259=CARTESIAN_POINT('Origin',(0.,0.35,0.));
#6260=CARTESIAN_POINT('Origin',(0.,0.45,0.));
#6261=CARTESIAN_POINT('Origin',(0.,0.35,0.));
#6262=CARTESIAN_POINT('Origin',(0.,0.45,0.));
#6263=CARTESIAN_POINT('Origin',(0.,0.35,0.));
#6264=CARTESIAN_POINT('Origin',(0.,0.45,0.));
#6265=CARTESIAN_POINT('Origin',(0.,0.35,0.));
#6266=CARTESIAN_POINT('Origin',(0.,0.45,0.));
#6267=CARTESIAN_POINT('Origin',(0.,0.35,0.));
#6268=CARTESIAN_POINT('Origin',(0.,0.45,0.));
#6269=CARTESIAN_POINT('Origin',(0.,0.35,0.));
#6270=CARTESIAN_POINT('Origin',(0.,0.45,0.));
#6271=CARTESIAN_POINT('Origin',(0.,0.35,0.));
#6272=CARTESIAN_POINT('Origin',(0.,0.45,0.));
#6273=CARTESIAN_POINT('Origin',(0.,0.35,0.));
#6274=CARTESIAN_POINT('Origin',(0.,0.45,0.));
#6275=CARTESIAN_POINT('Origin',(0.,0.35,0.));
#6276=CARTESIAN_POINT('Origin',(0.,0.45,0.));
#6277=CARTESIAN_POINT('Origin',(0.,0.35,0.));
#6278=CARTESIAN_POINT('Origin',(0.,0.45,0.));
#6279=CARTESIAN_POINT('Origin',(0.,0.35,0.));
#6280=CARTESIAN_POINT('Origin',(1.4,0.35,0.));
#6281=CARTESIAN_POINT('',(-1.4,0.35,-1.71450551880629E-16));
#6282=CARTESIAN_POINT('Origin',(0.,0.35,0.));
#6283=CARTESIAN_POINT('Origin',(0.,0.175,0.));
#6284=CARTESIAN_POINT('',(-1.4,0.,-1.71450551880629E-16));
#6285=CARTESIAN_POINT('Origin',(0.,0.,0.));
#6286=CARTESIAN_POINT('',(-1.4,0.175,-1.71450551880629E-16));
#6287=CARTESIAN_POINT('Origin',(0.75,0.,0.));
#6288=CARTESIAN_POINT('',(-0.75,0.,-9.18485099360515E-17));
#6289=CARTESIAN_POINT('Origin',(0.,0.,0.));
#6290=CARTESIAN_POINT('Origin',(0.,0.175,0.));
#6291=CARTESIAN_POINT('',(-0.75,0.175,-9.18485099360515E-17));
#7768=UNCERTAINTY_MEASURE_WITH_UNIT(LENGTH_MEASURE(0.001),#7817,
'DISTANCE_ACCURACY_VALUE',
'Maximum model space distance between geometric entities at asserted c
onnectivities');
#7789=UNCERTAINTY_MEASURE_WITH_UNIT(LENGTH_MEASURE(0.001),#7817,
'DISTANCE_ACCURACY_VALUE',
'Maximum model space distance between geometric entities at asserted c
onnectivities');
#7795=(
GEOMETRIC_REPRESENTATION_CONTEXT(3)
GLOBAL_UNCERTAINTY_ASSIGNED_CONTEXT((#7768))
GLOBAL_UNIT_ASSIGNED_CONTEXT((#7817,#7819,#7820))
REPRESENTATION_CONTEXT('','3D')
);
#7816=(
GEOMETRIC_REPRESENTATION_CONTEXT(3)
GLOBAL_UNCERTAINTY_ASSIGNED_CONTEXT((#7789))
GLOBAL_UNIT_ASSIGNED_CONTEXT((#7817,#7819,#7820))
REPRESENTATION_CONTEXT('','3D')
);
#7817=(
LENGTH_UNIT()
NAMED_UNIT(*)
SI_UNIT(.CENTI.,.METRE.)
);
#7819=(
NAMED_UNIT(*)
PLANE_ANGLE_UNIT()
SI_UNIT($,.RADIAN.)
);
#7820=(
NAMED_UNIT(*)
SI_UNIT($,.STERADIAN.)
SOLID_ANGLE_UNIT()
);
#7826=SHAPE_DEFINITION_REPRESENTATION(#7852,#7906);
#7852=PRODUCT_DEFINITION_SHAPE('',$,#7933);
#7906=SHAPE_REPRESENTATION('',(#4005),#7795);
#7927=PRODUCT_DEFINITION_CONTEXT('part definition',#8007,'design');
#7933=PRODUCT_DEFINITION('Shaft washer','Shaft washer',#7959,#7927);
#7959=PRODUCT_DEFINITION_FORMATION('',$,#8014);
#8007=APPLICATION_CONTEXT(
'Core Data for Automotive Mechanical Design Process');
#8008=PRODUCT_CONTEXT('part definition',#8007,'mechanical');
#8014=PRODUCT('Shaft washer','Shaft washer','Shaft washer',(#8008));
#8098=COLOUR_RGB('Black',0.12,0.14,0.17);
#8099=FILL_AREA_STYLE_COLOUR('',#8098);
#8100=FILL_AREA_STYLE('',(#8099));
#8101=SURFACE_STYLE_FILL_AREA(#8100);
#8102=SURFACE_SIDE_STYLE('',(#8101));
#8103=SURFACE_STYLE_USAGE(.BOTH.,#8102);
#8104=PRESENTATION_STYLE_ASSIGNMENT((#8103));
ENDSEC;
END-ISO-10303-21;
